ISO-10303-21;
HEADER;
/* Generated by software containing ST-Developer
 * from STEP Tools, Inc. (www.steptools.com) 
 */
/* OPTION: using custom renumber hook */

FILE_DESCRIPTION(
/* description */ ('STEP AP242 Edition 2', 'CAx-IF Rec.Pracs.---Representation and Presentation of Product Manufa
cturing Information (PMI)---4.0---2014-10-13', 'CAx-IF Rec.Pracs.---3D Tessellated Geometry---0.4---2014-09-14', '2;1', 'CAx-IF Rec.Pracs.---User Defined Attributes---1.5---2016-08-15'),
/* implementation_level */ '2;1');

FILE_NAME(
/* name */ 'Part 1__PD10213.step',
/* time_stamp */ '2026-10-09T13:59:33Z',
/* author */ (''),
/* organization */ (''),
/* preprocessor_version */ 'ST-DEVELOPER v20',
/* originating_system */ 'ONSHAPE BY PTC INC, 1.221',
/* authorisation */ '  ');

FILE_SCHEMA (('AP242_MANAGED_MODEL_BASED_3D_ENGINEERING_MIM_LF { 1 0 10303 442 3 1 4 }'));
ENDSEC;

DATA;
#39=LINE('',#8540,#323);
#40=LINE('',#8544,#324);
#41=LINE('',#8549,#325);
#42=LINE('',#8553,#326);
#43=LINE('',#8560,#327);
#44=LINE('',#8565,#328);
#45=LINE('',#8653,#329);
#46=LINE('',#8657,#330);
#47=LINE('',#8661,#331);
#48=LINE('',#8673,#332);
#49=LINE('',#8677,#333);
#50=LINE('',#8681,#334);
#51=LINE('',#8768,#335);
#52=LINE('',#8772,#336);
#53=LINE('',#8774,#337);
#54=LINE('',#8776,#338);
#55=LINE('',#8778,#339);
#56=LINE('',#8780,#340);
#57=LINE('',#8782,#341);
#58=LINE('',#8784,#342);
#59=LINE('',#8787,#343);
#60=LINE('',#8788,#344);
#61=LINE('',#8790,#345);
#62=LINE('',#8792,#346);
#63=LINE('',#8795,#347);
#64=LINE('',#8796,#348);
#65=LINE('',#8798,#349);
#66=LINE('',#8799,#350);
#67=LINE('',#8801,#351);
#68=LINE('',#8802,#352);
#69=LINE('',#8804,#353);
#70=LINE('',#8805,#354);
#71=LINE('',#8807,#355);
#72=LINE('',#8808,#356);
#73=LINE('',#8810,#357);
#74=LINE('',#8811,#358);
#75=LINE('',#8813,#359);
#76=LINE('',#8814,#360);
#77=LINE('',#8816,#361);
#78=LINE('',#8817,#362);
#79=LINE('',#8819,#363);
#80=LINE('',#8820,#364);
#81=LINE('',#8822,#365);
#82=LINE('',#8823,#366);
#83=LINE('',#8825,#367);
#84=LINE('',#8827,#368);
#85=LINE('',#8830,#369);
#86=LINE('',#8832,#370);
#87=LINE('',#8835,#371);
#88=LINE('',#8837,#372);
#89=LINE('',#8840,#373);
#90=LINE('',#8842,#374);
#91=LINE('',#8845,#375);
#92=LINE('',#8847,#376);
#93=LINE('',#8850,#377);
#94=LINE('',#8852,#378);
#95=LINE('',#8855,#379);
#96=LINE('',#8857,#380);
#97=LINE('',#8860,#381);
#98=LINE('',#8862,#382);
#99=LINE('',#8865,#383);
#100=LINE('',#8867,#384);
#101=LINE('',#8870,#385);
#102=LINE('',#8872,#386);
#103=LINE('',#8875,#387);
#104=LINE('',#8877,#388);
#323=VECTOR('',#6621,1.);
#324=VECTOR('',#6624,1.);
#325=VECTOR('',#6629,1.);
#326=VECTOR('',#6632,1.);
#327=VECTOR('',#6641,1.);
#328=VECTOR('',#6644,1.);
#329=VECTOR('',#6733,1.);
#330=VECTOR('',#6736,1.);
#331=VECTOR('',#6739,1.);
#332=VECTOR('',#6752,1.);
#333=VECTOR('',#6755,1.);
#334=VECTOR('',#6758,1.);
#335=VECTOR('',#6845,1.);
#336=VECTOR('',#6848,1.);
#337=VECTOR('',#6851,1.);
#338=VECTOR('',#6854,1.);
#339=VECTOR('',#6857,1.);
#340=VECTOR('',#6860,1.);
#341=VECTOR('',#6863,1.);
#342=VECTOR('',#6866,1.);
#343=VECTOR('',#6871,1.);
#344=VECTOR('',#6872,1.);
#345=VECTOR('',#6875,1.);
#346=VECTOR('',#6878,1.);
#347=VECTOR('',#6883,1.);
#348=VECTOR('',#6884,1.);
#349=VECTOR('',#6887,1.);
#350=VECTOR('',#6888,1.);
#351=VECTOR('',#6891,1.);
#352=VECTOR('',#6892,1.);
#353=VECTOR('',#6895,1.);
#354=VECTOR('',#6896,1.);
#355=VECTOR('',#6899,1.);
#356=VECTOR('',#6900,1.);
#357=VECTOR('',#6903,1.);
#358=VECTOR('',#6904,1.);
#359=VECTOR('',#6907,1.);
#360=VECTOR('',#6908,1.);
#361=VECTOR('',#6911,1.);
#362=VECTOR('',#6912,1.);
#363=VECTOR('',#6915,1.);
#364=VECTOR('',#6916,1.);
#365=VECTOR('',#6919,1.);
#366=VECTOR('',#6920,1.);
#367=VECTOR('',#6923,1.);
#368=VECTOR('',#6926,1.);
#369=VECTOR('',#6931,1.);
#370=VECTOR('',#6934,1.);
#371=VECTOR('',#6939,1.);
#372=VECTOR('',#6942,1.);
#373=VECTOR('',#6947,1.);
#374=VECTOR('',#6950,1.);
#375=VECTOR('',#6955,1.);
#376=VECTOR('',#6958,1.);
#377=VECTOR('',#6963,1.);
#378=VECTOR('',#6966,1.);
#379=VECTOR('',#6971,1.);
#380=VECTOR('',#6974,1.);
#381=VECTOR('',#6979,1.);
#382=VECTOR('',#6982,1.);
#383=VECTOR('',#6987,1.);
#384=VECTOR('',#6990,1.);
#385=VECTOR('',#6995,1.);
#386=VECTOR('',#6998,1.);
#387=VECTOR('',#7003,1.);
#388=VECTOR('',#7006,1.);
#673=SHAPE_REPRESENTATION_RELATIONSHIP('','',#5691,#687);
#687=ADVANCED_BREP_SHAPE_REPRESENTATION('',(#5660),#10145);
#710=PLANE('',#5767);
#711=PLANE('',#5817);
#712=PLANE('',#5867);
#713=PLANE('',#5870);
#714=PLANE('',#5872);
#715=PLANE('',#5875);
#716=PLANE('',#5877);
#892=ORIENTED_EDGE('',*,*,#2383,.T.);
#893=ORIENTED_EDGE('',*,*,#2384,.F.);
#894=ORIENTED_EDGE('',*,*,#2385,.F.);
#895=ORIENTED_EDGE('',*,*,#2386,.T.);
#896=ORIENTED_EDGE('',*,*,#2387,.F.);
#897=ORIENTED_EDGE('',*,*,#2388,.F.);
#898=ORIENTED_EDGE('',*,*,#2389,.T.);
#899=ORIENTED_EDGE('',*,*,#2390,.F.);
#900=ORIENTED_EDGE('',*,*,#2391,.F.);
#901=ORIENTED_EDGE('',*,*,#2392,.T.);
#902=ORIENTED_EDGE('',*,*,#2392,.F.);
#903=ORIENTED_EDGE('',*,*,#2393,.F.);
#904=ORIENTED_EDGE('',*,*,#2394,.F.);
#905=ORIENTED_EDGE('',*,*,#2395,.F.);
#906=ORIENTED_EDGE('',*,*,#2396,.F.);
#907=ORIENTED_EDGE('',*,*,#2385,.T.);
#908=ORIENTED_EDGE('',*,*,#2397,.F.);
#909=ORIENTED_EDGE('',*,*,#2398,.F.);
#910=ORIENTED_EDGE('',*,*,#2399,.F.);
#911=ORIENTED_EDGE('',*,*,#2400,.T.);
#912=ORIENTED_EDGE('',*,*,#2401,.F.);
#913=ORIENTED_EDGE('',*,*,#2402,.F.);
#914=ORIENTED_EDGE('',*,*,#2403,.F.);
#915=ORIENTED_EDGE('',*,*,#2404,.T.);
#916=ORIENTED_EDGE('',*,*,#2405,.F.);
#917=ORIENTED_EDGE('',*,*,#2406,.F.);
#918=ORIENTED_EDGE('',*,*,#2407,.F.);
#919=ORIENTED_EDGE('',*,*,#2408,.T.);
#920=ORIENTED_EDGE('',*,*,#2409,.F.);
#921=ORIENTED_EDGE('',*,*,#2410,.F.);
#922=ORIENTED_EDGE('',*,*,#2411,.F.);
#923=ORIENTED_EDGE('',*,*,#2412,.T.);
#924=ORIENTED_EDGE('',*,*,#2413,.F.);
#925=ORIENTED_EDGE('',*,*,#2414,.F.);
#926=ORIENTED_EDGE('',*,*,#2415,.F.);
#927=ORIENTED_EDGE('',*,*,#2416,.T.);
#928=ORIENTED_EDGE('',*,*,#2417,.F.);
#929=ORIENTED_EDGE('',*,*,#2418,.F.);
#930=ORIENTED_EDGE('',*,*,#2419,.F.);
#931=ORIENTED_EDGE('',*,*,#2420,.T.);
#932=ORIENTED_EDGE('',*,*,#2421,.F.);
#933=ORIENTED_EDGE('',*,*,#2422,.F.);
#934=ORIENTED_EDGE('',*,*,#2423,.F.);
#935=ORIENTED_EDGE('',*,*,#2424,.T.);
#936=ORIENTED_EDGE('',*,*,#2425,.F.);
#937=ORIENTED_EDGE('',*,*,#2426,.F.);
#938=ORIENTED_EDGE('',*,*,#2427,.F.);
#939=ORIENTED_EDGE('',*,*,#2428,.T.);
#940=ORIENTED_EDGE('',*,*,#2429,.F.);
#941=ORIENTED_EDGE('',*,*,#2430,.F.);
#942=ORIENTED_EDGE('',*,*,#2431,.F.);
#943=ORIENTED_EDGE('',*,*,#2432,.T.);
#944=ORIENTED_EDGE('',*,*,#2433,.F.);
#945=ORIENTED_EDGE('',*,*,#2434,.F.);
#946=ORIENTED_EDGE('',*,*,#2435,.F.);
#947=ORIENTED_EDGE('',*,*,#2436,.T.);
#948=ORIENTED_EDGE('',*,*,#2437,.F.);
#949=ORIENTED_EDGE('',*,*,#2438,.F.);
#950=ORIENTED_EDGE('',*,*,#2439,.F.);
#951=ORIENTED_EDGE('',*,*,#2387,.T.);
#952=ORIENTED_EDGE('',*,*,#2440,.T.);
#953=ORIENTED_EDGE('',*,*,#2441,.T.);
#954=ORIENTED_EDGE('',*,*,#2442,.T.);
#955=ORIENTED_EDGE('',*,*,#2443,.T.);
#956=ORIENTED_EDGE('',*,*,#2444,.T.);
#957=ORIENTED_EDGE('',*,*,#2445,.T.);
#958=ORIENTED_EDGE('',*,*,#2446,.T.);
#959=ORIENTED_EDGE('',*,*,#2391,.T.);
#960=ORIENTED_EDGE('',*,*,#2447,.F.);
#961=ORIENTED_EDGE('',*,*,#2383,.F.);
#962=ORIENTED_EDGE('',*,*,#2448,.F.);
#963=ORIENTED_EDGE('',*,*,#2449,.F.);
#964=ORIENTED_EDGE('',*,*,#2450,.F.);
#965=ORIENTED_EDGE('',*,*,#2451,.F.);
#966=ORIENTED_EDGE('',*,*,#2452,.F.);
#967=ORIENTED_EDGE('',*,*,#2453,.F.);
#968=ORIENTED_EDGE('',*,*,#2454,.F.);
#969=ORIENTED_EDGE('',*,*,#2389,.F.);
#970=ORIENTED_EDGE('',*,*,#2455,.F.);
#971=ORIENTED_EDGE('',*,*,#2456,.F.);
#972=ORIENTED_EDGE('',*,*,#2457,.F.);
#973=ORIENTED_EDGE('',*,*,#2458,.F.);
#974=ORIENTED_EDGE('',*,*,#2459,.F.);
#975=ORIENTED_EDGE('',*,*,#2460,.F.);
#976=ORIENTED_EDGE('',*,*,#2461,.F.);
#977=ORIENTED_EDGE('',*,*,#2462,.F.);
#978=ORIENTED_EDGE('',*,*,#2463,.F.);
#979=ORIENTED_EDGE('',*,*,#2464,.F.);
#980=ORIENTED_EDGE('',*,*,#2465,.F.);
#981=ORIENTED_EDGE('',*,*,#2466,.F.);
#982=ORIENTED_EDGE('',*,*,#2467,.F.);
#983=ORIENTED_EDGE('',*,*,#2468,.F.);
#984=ORIENTED_EDGE('',*,*,#2469,.F.);
#985=ORIENTED_EDGE('',*,*,#2470,.F.);
#986=ORIENTED_EDGE('',*,*,#2471,.F.);
#987=ORIENTED_EDGE('',*,*,#2472,.F.);
#988=ORIENTED_EDGE('',*,*,#2473,.F.);
#989=ORIENTED_EDGE('',*,*,#2474,.F.);
#990=ORIENTED_EDGE('',*,*,#2475,.F.);
#991=ORIENTED_EDGE('',*,*,#2476,.F.);
#992=ORIENTED_EDGE('',*,*,#2477,.F.);
#993=ORIENTED_EDGE('',*,*,#2478,.F.);
#994=ORIENTED_EDGE('',*,*,#2479,.F.);
#995=ORIENTED_EDGE('',*,*,#2480,.F.);
#996=ORIENTED_EDGE('',*,*,#2481,.F.);
#997=ORIENTED_EDGE('',*,*,#2482,.F.);
#998=ORIENTED_EDGE('',*,*,#2483,.F.);
#999=ORIENTED_EDGE('',*,*,#2484,.F.);
#1000=ORIENTED_EDGE('',*,*,#2485,.F.);
#1001=ORIENTED_EDGE('',*,*,#2486,.F.);
#1002=ORIENTED_EDGE('',*,*,#2487,.F.);
#1003=ORIENTED_EDGE('',*,*,#2488,.F.);
#1004=ORIENTED_EDGE('',*,*,#2489,.F.);
#1005=ORIENTED_EDGE('',*,*,#2490,.F.);
#1006=ORIENTED_EDGE('',*,*,#2491,.F.);
#1007=ORIENTED_EDGE('',*,*,#2492,.F.);
#1008=ORIENTED_EDGE('',*,*,#2493,.F.);
#1009=ORIENTED_EDGE('',*,*,#2494,.F.);
#1010=ORIENTED_EDGE('',*,*,#2495,.F.);
#1011=ORIENTED_EDGE('',*,*,#2496,.F.);
#1012=ORIENTED_EDGE('',*,*,#2497,.T.);
#1013=ORIENTED_EDGE('',*,*,#2498,.T.);
#1014=ORIENTED_EDGE('',*,*,#2499,.T.);
#1015=ORIENTED_EDGE('',*,*,#2500,.T.);
#1016=ORIENTED_EDGE('',*,*,#2454,.T.);
#1017=ORIENTED_EDGE('',*,*,#2501,.F.);
#1018=ORIENTED_EDGE('',*,*,#2440,.F.);
#1019=ORIENTED_EDGE('',*,*,#2390,.T.);
#1020=ORIENTED_EDGE('',*,*,#2448,.T.);
#1021=ORIENTED_EDGE('',*,*,#2386,.F.);
#1022=ORIENTED_EDGE('',*,*,#2446,.F.);
#1023=ORIENTED_EDGE('',*,*,#2502,.T.);
#1024=ORIENTED_EDGE('',*,*,#2449,.T.);
#1025=ORIENTED_EDGE('',*,*,#2502,.F.);
#1026=ORIENTED_EDGE('',*,*,#2445,.F.);
#1027=ORIENTED_EDGE('',*,*,#2503,.T.);
#1028=ORIENTED_EDGE('',*,*,#2450,.T.);
#1029=ORIENTED_EDGE('',*,*,#2503,.F.);
#1030=ORIENTED_EDGE('',*,*,#2444,.F.);
#1031=ORIENTED_EDGE('',*,*,#2504,.T.);
#1032=ORIENTED_EDGE('',*,*,#2451,.T.);
#1033=ORIENTED_EDGE('',*,*,#2504,.F.);
#1034=ORIENTED_EDGE('',*,*,#2443,.F.);
#1035=ORIENTED_EDGE('',*,*,#2505,.T.);
#1036=ORIENTED_EDGE('',*,*,#2452,.T.);
#1037=ORIENTED_EDGE('',*,*,#2505,.F.);
#1038=ORIENTED_EDGE('',*,*,#2442,.F.);
#1039=ORIENTED_EDGE('',*,*,#2506,.T.);
#1040=ORIENTED_EDGE('',*,*,#2453,.T.);
#1041=ORIENTED_EDGE('',*,*,#2506,.F.);
#1042=ORIENTED_EDGE('',*,*,#2441,.F.);
#1043=ORIENTED_EDGE('',*,*,#2501,.T.);
#1044=ORIENTED_EDGE('',*,*,#2497,.F.);
#1045=ORIENTED_EDGE('',*,*,#2507,.F.);
#1046=ORIENTED_EDGE('',*,*,#2394,.T.);
#1047=ORIENTED_EDGE('',*,*,#2508,.T.);
#1048=ORIENTED_EDGE('',*,*,#2498,.F.);
#1049=ORIENTED_EDGE('',*,*,#2508,.F.);
#1050=ORIENTED_EDGE('',*,*,#2393,.T.);
#1051=ORIENTED_EDGE('',*,*,#2509,.T.);
#1052=ORIENTED_EDGE('',*,*,#2499,.F.);
#1053=ORIENTED_EDGE('',*,*,#2509,.F.);
#1054=ORIENTED_EDGE('',*,*,#2396,.T.);
#1055=ORIENTED_EDGE('',*,*,#2510,.T.);
#1056=ORIENTED_EDGE('',*,*,#2500,.F.);
#1057=ORIENTED_EDGE('',*,*,#2510,.F.);
#1058=ORIENTED_EDGE('',*,*,#2395,.T.);
#1059=ORIENTED_EDGE('',*,*,#2507,.T.);
#1060=ORIENTED_EDGE('',*,*,#2511,.F.);
#1061=ORIENTED_EDGE('',*,*,#2458,.T.);
#1062=ORIENTED_EDGE('',*,*,#2512,.F.);
#1063=ORIENTED_EDGE('',*,*,#2436,.F.);
#1064=ORIENTED_EDGE('',*,*,#2513,.F.);
#1065=ORIENTED_EDGE('',*,*,#2462,.T.);
#1066=ORIENTED_EDGE('',*,*,#2514,.F.);
#1067=ORIENTED_EDGE('',*,*,#2432,.F.);
#1068=ORIENTED_EDGE('',*,*,#2515,.F.);
#1069=ORIENTED_EDGE('',*,*,#2428,.F.);
#1070=ORIENTED_EDGE('',*,*,#2516,.F.);
#1071=ORIENTED_EDGE('',*,*,#2466,.T.);
#1072=ORIENTED_EDGE('',*,*,#2517,.F.);
#1073=ORIENTED_EDGE('',*,*,#2424,.F.);
#1074=ORIENTED_EDGE('',*,*,#2518,.F.);
#1075=ORIENTED_EDGE('',*,*,#2470,.T.);
#1076=ORIENTED_EDGE('',*,*,#2519,.F.);
#1077=ORIENTED_EDGE('',*,*,#2474,.T.);
#1078=ORIENTED_EDGE('',*,*,#2520,.F.);
#1079=ORIENTED_EDGE('',*,*,#2420,.F.);
#1080=ORIENTED_EDGE('',*,*,#2521,.F.);
#1081=ORIENTED_EDGE('',*,*,#2478,.T.);
#1082=ORIENTED_EDGE('',*,*,#2522,.F.);
#1083=ORIENTED_EDGE('',*,*,#2416,.F.);
#1084=ORIENTED_EDGE('',*,*,#2523,.F.);
#1085=ORIENTED_EDGE('',*,*,#2412,.F.);
#1086=ORIENTED_EDGE('',*,*,#2524,.F.);
#1087=ORIENTED_EDGE('',*,*,#2482,.T.);
#1088=ORIENTED_EDGE('',*,*,#2525,.F.);
#1089=ORIENTED_EDGE('',*,*,#2486,.T.);
#1090=ORIENTED_EDGE('',*,*,#2526,.F.);
#1091=ORIENTED_EDGE('',*,*,#2408,.F.);
#1092=ORIENTED_EDGE('',*,*,#2527,.F.);
#1093=ORIENTED_EDGE('',*,*,#2490,.T.);
#1094=ORIENTED_EDGE('',*,*,#2528,.F.);
#1095=ORIENTED_EDGE('',*,*,#2404,.F.);
#1096=ORIENTED_EDGE('',*,*,#2529,.F.);
#1097=ORIENTED_EDGE('',*,*,#2494,.T.);
#1098=ORIENTED_EDGE('',*,*,#2530,.F.);
#1099=ORIENTED_EDGE('',*,*,#2400,.F.);
#1100=ORIENTED_EDGE('',*,*,#2384,.T.);
#1101=ORIENTED_EDGE('',*,*,#2447,.T.);
#1102=ORIENTED_EDGE('',*,*,#2531,.F.);
#1103=ORIENTED_EDGE('',*,*,#2397,.T.);
#1104=ORIENTED_EDGE('',*,*,#2531,.T.);
#1105=ORIENTED_EDGE('',*,*,#2496,.T.);
#1106=ORIENTED_EDGE('',*,*,#2532,.F.);
#1107=ORIENTED_EDGE('',*,*,#2398,.T.);
#1108=ORIENTED_EDGE('',*,*,#2532,.T.);
#1109=ORIENTED_EDGE('',*,*,#2495,.T.);
#1110=ORIENTED_EDGE('',*,*,#2529,.T.);
#1111=ORIENTED_EDGE('',*,*,#2399,.T.);
#1112=ORIENTED_EDGE('',*,*,#2530,.T.);
#1113=ORIENTED_EDGE('',*,*,#2493,.T.);
#1114=ORIENTED_EDGE('',*,*,#2533,.F.);
#1115=ORIENTED_EDGE('',*,*,#2401,.T.);
#1116=ORIENTED_EDGE('',*,*,#2533,.T.);
#1117=ORIENTED_EDGE('',*,*,#2492,.T.);
#1118=ORIENTED_EDGE('',*,*,#2534,.F.);
#1119=ORIENTED_EDGE('',*,*,#2402,.T.);
#1120=ORIENTED_EDGE('',*,*,#2534,.T.);
#1121=ORIENTED_EDGE('',*,*,#2491,.T.);
#1122=ORIENTED_EDGE('',*,*,#2527,.T.);
#1123=ORIENTED_EDGE('',*,*,#2403,.T.);
#1124=ORIENTED_EDGE('',*,*,#2528,.T.);
#1125=ORIENTED_EDGE('',*,*,#2489,.T.);
#1126=ORIENTED_EDGE('',*,*,#2535,.F.);
#1127=ORIENTED_EDGE('',*,*,#2405,.T.);
#1128=ORIENTED_EDGE('',*,*,#2535,.T.);
#1129=ORIENTED_EDGE('',*,*,#2488,.T.);
#1130=ORIENTED_EDGE('',*,*,#2536,.F.);
#1131=ORIENTED_EDGE('',*,*,#2406,.T.);
#1132=ORIENTED_EDGE('',*,*,#2536,.T.);
#1133=ORIENTED_EDGE('',*,*,#2487,.T.);
#1134=ORIENTED_EDGE('',*,*,#2525,.T.);
#1135=ORIENTED_EDGE('',*,*,#2407,.T.);
#1136=ORIENTED_EDGE('',*,*,#2526,.T.);
#1137=ORIENTED_EDGE('',*,*,#2485,.T.);
#1138=ORIENTED_EDGE('',*,*,#2537,.F.);
#1139=ORIENTED_EDGE('',*,*,#2409,.T.);
#1140=ORIENTED_EDGE('',*,*,#2537,.T.);
#1141=ORIENTED_EDGE('',*,*,#2484,.T.);
#1142=ORIENTED_EDGE('',*,*,#2538,.F.);
#1143=ORIENTED_EDGE('',*,*,#2410,.T.);
#1144=ORIENTED_EDGE('',*,*,#2538,.T.);
#1145=ORIENTED_EDGE('',*,*,#2483,.T.);
#1146=ORIENTED_EDGE('',*,*,#2524,.T.);
#1147=ORIENTED_EDGE('',*,*,#2411,.T.);
#1148=ORIENTED_EDGE('',*,*,#2523,.T.);
#1149=ORIENTED_EDGE('',*,*,#2481,.T.);
#1150=ORIENTED_EDGE('',*,*,#2539,.F.);
#1151=ORIENTED_EDGE('',*,*,#2413,.T.);
#1152=ORIENTED_EDGE('',*,*,#2539,.T.);
#1153=ORIENTED_EDGE('',*,*,#2480,.T.);
#1154=ORIENTED_EDGE('',*,*,#2540,.F.);
#1155=ORIENTED_EDGE('',*,*,#2414,.T.);
#1156=ORIENTED_EDGE('',*,*,#2540,.T.);
#1157=ORIENTED_EDGE('',*,*,#2479,.T.);
#1158=ORIENTED_EDGE('',*,*,#2521,.T.);
#1159=ORIENTED_EDGE('',*,*,#2415,.T.);
#1160=ORIENTED_EDGE('',*,*,#2522,.T.);
#1161=ORIENTED_EDGE('',*,*,#2477,.T.);
#1162=ORIENTED_EDGE('',*,*,#2541,.F.);
#1163=ORIENTED_EDGE('',*,*,#2417,.T.);
#1164=ORIENTED_EDGE('',*,*,#2541,.T.);
#1165=ORIENTED_EDGE('',*,*,#2476,.T.);
#1166=ORIENTED_EDGE('',*,*,#2542,.F.);
#1167=ORIENTED_EDGE('',*,*,#2418,.T.);
#1168=ORIENTED_EDGE('',*,*,#2542,.T.);
#1169=ORIENTED_EDGE('',*,*,#2475,.T.);
#1170=ORIENTED_EDGE('',*,*,#2519,.T.);
#1171=ORIENTED_EDGE('',*,*,#2419,.T.);
#1172=ORIENTED_EDGE('',*,*,#2520,.T.);
#1173=ORIENTED_EDGE('',*,*,#2473,.T.);
#1174=ORIENTED_EDGE('',*,*,#2543,.F.);
#1175=ORIENTED_EDGE('',*,*,#2421,.T.);
#1176=ORIENTED_EDGE('',*,*,#2543,.T.);
#1177=ORIENTED_EDGE('',*,*,#2472,.T.);
#1178=ORIENTED_EDGE('',*,*,#2544,.F.);
#1179=ORIENTED_EDGE('',*,*,#2422,.T.);
#1180=ORIENTED_EDGE('',*,*,#2544,.T.);
#1181=ORIENTED_EDGE('',*,*,#2471,.T.);
#1182=ORIENTED_EDGE('',*,*,#2518,.T.);
#1183=ORIENTED_EDGE('',*,*,#2423,.T.);
#1184=ORIENTED_EDGE('',*,*,#2517,.T.);
#1185=ORIENTED_EDGE('',*,*,#2469,.T.);
#1186=ORIENTED_EDGE('',*,*,#2545,.F.);
#1187=ORIENTED_EDGE('',*,*,#2425,.T.);
#1188=ORIENTED_EDGE('',*,*,#2545,.T.);
#1189=ORIENTED_EDGE('',*,*,#2468,.T.);
#1190=ORIENTED_EDGE('',*,*,#2546,.F.);
#1191=ORIENTED_EDGE('',*,*,#2426,.T.);
#1192=ORIENTED_EDGE('',*,*,#2546,.T.);
#1193=ORIENTED_EDGE('',*,*,#2467,.T.);
#1194=ORIENTED_EDGE('',*,*,#2516,.T.);
#1195=ORIENTED_EDGE('',*,*,#2427,.T.);
#1196=ORIENTED_EDGE('',*,*,#2515,.T.);
#1197=ORIENTED_EDGE('',*,*,#2465,.T.);
#1198=ORIENTED_EDGE('',*,*,#2547,.F.);
#1199=ORIENTED_EDGE('',*,*,#2429,.T.);
#1200=ORIENTED_EDGE('',*,*,#2547,.T.);
#1201=ORIENTED_EDGE('',*,*,#2464,.T.);
#1202=ORIENTED_EDGE('',*,*,#2548,.F.);
#1203=ORIENTED_EDGE('',*,*,#2430,.T.);
#1204=ORIENTED_EDGE('',*,*,#2548,.T.);
#1205=ORIENTED_EDGE('',*,*,#2463,.T.);
#1206=ORIENTED_EDGE('',*,*,#2513,.T.);
#1207=ORIENTED_EDGE('',*,*,#2431,.T.);
#1208=ORIENTED_EDGE('',*,*,#2514,.T.);
#1209=ORIENTED_EDGE('',*,*,#2461,.T.);
#1210=ORIENTED_EDGE('',*,*,#2549,.F.);
#1211=ORIENTED_EDGE('',*,*,#2433,.T.);
#1212=ORIENTED_EDGE('',*,*,#2549,.T.);
#1213=ORIENTED_EDGE('',*,*,#2460,.T.);
#1214=ORIENTED_EDGE('',*,*,#2550,.F.);
#1215=ORIENTED_EDGE('',*,*,#2434,.T.);
#1216=ORIENTED_EDGE('',*,*,#2550,.T.);
#1217=ORIENTED_EDGE('',*,*,#2459,.T.);
#1218=ORIENTED_EDGE('',*,*,#2511,.T.);
#1219=ORIENTED_EDGE('',*,*,#2435,.T.);
#1220=ORIENTED_EDGE('',*,*,#2512,.T.);
#1221=ORIENTED_EDGE('',*,*,#2457,.T.);
#1222=ORIENTED_EDGE('',*,*,#2551,.F.);
#1223=ORIENTED_EDGE('',*,*,#2437,.T.);
#1224=ORIENTED_EDGE('',*,*,#2551,.T.);
#1225=ORIENTED_EDGE('',*,*,#2456,.T.);
#1226=ORIENTED_EDGE('',*,*,#2552,.F.);
#1227=ORIENTED_EDGE('',*,*,#2438,.T.);
#1228=ORIENTED_EDGE('',*,*,#2552,.T.);
#1229=ORIENTED_EDGE('',*,*,#2455,.T.);
#1230=ORIENTED_EDGE('',*,*,#2388,.T.);
#1231=ORIENTED_EDGE('',*,*,#2439,.T.);
#2383=EDGE_CURVE('',#3142,#3143,#3675,.T.);
#2384=EDGE_CURVE('',#3144,#3143,#39,.T.);
#2385=EDGE_CURVE('',#3145,#3144,#3676,.T.);
#2386=EDGE_CURVE('',#3145,#3142,#40,.T.);
#2387=EDGE_CURVE('',#3146,#3147,#3677,.T.);
#2388=EDGE_CURVE('',#3148,#3146,#41,.F.);
#2389=EDGE_CURVE('',#3148,#3149,#3678,.T.);
#2390=EDGE_CURVE('',#3147,#3149,#42,.T.);
#2391=EDGE_CURVE('',#3150,#3150,#3679,.T.);
#2392=EDGE_CURVE('',#3151,#3151,#3680,.T.);
#2393=EDGE_CURVE('',#3152,#3153,#43,.T.);
#2394=EDGE_CURVE('',#3154,#3152,#3681,.T.);
#2395=EDGE_CURVE('',#3155,#3154,#44,.T.);
#2396=EDGE_CURVE('',#3153,#3155,#3682,.T.);
#2397=EDGE_CURVE('',#3156,#3144,#3683,.T.);
#2398=EDGE_CURVE('',#3157,#3156,#3684,.T.);
#2399=EDGE_CURVE('',#3158,#3157,#3685,.T.);
#2400=EDGE_CURVE('',#3158,#3159,#3686,.T.);
#2401=EDGE_CURVE('',#3160,#3159,#3687,.T.);
#2402=EDGE_CURVE('',#3161,#3160,#3688,.T.);
#2403=EDGE_CURVE('',#3162,#3161,#3689,.T.);
#2404=EDGE_CURVE('',#3162,#3163,#3690,.T.);
#2405=EDGE_CURVE('',#3164,#3163,#3691,.T.);
#2406=EDGE_CURVE('',#3165,#3164,#3692,.T.);
#2407=EDGE_CURVE('',#3166,#3165,#3693,.T.);
#2408=EDGE_CURVE('',#3166,#3167,#3694,.T.);
#2409=EDGE_CURVE('',#3168,#3167,#3695,.T.);
#2410=EDGE_CURVE('',#3169,#3168,#3696,.T.);
#2411=EDGE_CURVE('',#3170,#3169,#3697,.T.);
#2412=EDGE_CURVE('',#3170,#3171,#3698,.T.);
#2413=EDGE_CURVE('',#3172,#3171,#3699,.T.);
#2414=EDGE_CURVE('',#3173,#3172,#3700,.T.);
#2415=EDGE_CURVE('',#3174,#3173,#3701,.T.);
#2416=EDGE_CURVE('',#3174,#3175,#3702,.T.);
#2417=EDGE_CURVE('',#3176,#3175,#3703,.T.);
#2418=EDGE_CURVE('',#3177,#3176,#3704,.T.);
#2419=EDGE_CURVE('',#3178,#3177,#3705,.T.);
#2420=EDGE_CURVE('',#3178,#3179,#3706,.T.);
#2421=EDGE_CURVE('',#3180,#3179,#3707,.T.);
#2422=EDGE_CURVE('',#3181,#3180,#3708,.T.);
#2423=EDGE_CURVE('',#3182,#3181,#3709,.T.);
#2424=EDGE_CURVE('',#3182,#3183,#3710,.T.);
#2425=EDGE_CURVE('',#3184,#3183,#3711,.T.);
#2426=EDGE_CURVE('',#3185,#3184,#3712,.T.);
#2427=EDGE_CURVE('',#3186,#3185,#3713,.T.);
#2428=EDGE_CURVE('',#3186,#3187,#3714,.T.);
#2429=EDGE_CURVE('',#3188,#3187,#3715,.T.);
#2430=EDGE_CURVE('',#3189,#3188,#3716,.T.);
#2431=EDGE_CURVE('',#3190,#3189,#3717,.T.);
#2432=EDGE_CURVE('',#3190,#3191,#3718,.T.);
#2433=EDGE_CURVE('',#3192,#3191,#3719,.T.);
#2434=EDGE_CURVE('',#3193,#3192,#3720,.T.);
#2435=EDGE_CURVE('',#3194,#3193,#3721,.T.);
#2436=EDGE_CURVE('',#3194,#3195,#3722,.T.);
#2437=EDGE_CURVE('',#3196,#3195,#3723,.T.);
#2438=EDGE_CURVE('',#3197,#3196,#3724,.T.);
#2439=EDGE_CURVE('',#3146,#3197,#3725,.T.);
#2440=EDGE_CURVE('',#3147,#3198,#45,.T.);
#2441=EDGE_CURVE('',#3198,#3199,#3726,.T.);
#2442=EDGE_CURVE('',#3199,#3200,#46,.T.);
#2443=EDGE_CURVE('',#3200,#3201,#3727,.T.);
#2444=EDGE_CURVE('',#3201,#3202,#47,.T.);
#2445=EDGE_CURVE('',#3202,#3203,#3728,.T.);
#2446=EDGE_CURVE('',#3203,#3145,#3729,.T.);
#2447=EDGE_CURVE('',#3143,#3204,#3730,.T.);
#2448=EDGE_CURVE('',#3205,#3142,#3731,.T.);
#2449=EDGE_CURVE('',#3206,#3205,#3732,.T.);
#2450=EDGE_CURVE('',#3207,#3206,#48,.T.);
#2451=EDGE_CURVE('',#3208,#3207,#3733,.T.);
#2452=EDGE_CURVE('',#3209,#3208,#49,.T.);
#2453=EDGE_CURVE('',#3210,#3209,#3734,.T.);
#2454=EDGE_CURVE('',#3149,#3210,#50,.T.);
#2455=EDGE_CURVE('',#3211,#3148,#3735,.T.);
#2456=EDGE_CURVE('',#3212,#3211,#3736,.T.);
#2457=EDGE_CURVE('',#3213,#3212,#3737,.T.);
#2458=EDGE_CURVE('',#3214,#3213,#3738,.T.);
#2459=EDGE_CURVE('',#3215,#3214,#3739,.T.);
#2460=EDGE_CURVE('',#3216,#3215,#3740,.T.);
#2461=EDGE_CURVE('',#3217,#3216,#3741,.T.);
#2462=EDGE_CURVE('',#3218,#3217,#3742,.T.);
#2463=EDGE_CURVE('',#3219,#3218,#3743,.T.);
#2464=EDGE_CURVE('',#3220,#3219,#3744,.T.);
#2465=EDGE_CURVE('',#3221,#3220,#3745,.T.);
#2466=EDGE_CURVE('',#3222,#3221,#3746,.T.);
#2467=EDGE_CURVE('',#3223,#3222,#3747,.T.);
#2468=EDGE_CURVE('',#3224,#3223,#3748,.T.);
#2469=EDGE_CURVE('',#3225,#3224,#3749,.T.);
#2470=EDGE_CURVE('',#3226,#3225,#3750,.T.);
#2471=EDGE_CURVE('',#3227,#3226,#3751,.T.);
#2472=EDGE_CURVE('',#3228,#3227,#3752,.T.);
#2473=EDGE_CURVE('',#3229,#3228,#3753,.T.);
#2474=EDGE_CURVE('',#3230,#3229,#3754,.T.);
#2475=EDGE_CURVE('',#3231,#3230,#3755,.T.);
#2476=EDGE_CURVE('',#3232,#3231,#3756,.T.);
#2477=EDGE_CURVE('',#3233,#3232,#3757,.T.);
#2478=EDGE_CURVE('',#3234,#3233,#3758,.T.);
#2479=EDGE_CURVE('',#3235,#3234,#3759,.T.);
#2480=EDGE_CURVE('',#3236,#3235,#3760,.T.);
#2481=EDGE_CURVE('',#3237,#3236,#3761,.T.);
#2482=EDGE_CURVE('',#3238,#3237,#3762,.T.);
#2483=EDGE_CURVE('',#3239,#3238,#3763,.T.);
#2484=EDGE_CURVE('',#3240,#3239,#3764,.T.);
#2485=EDGE_CURVE('',#3241,#3240,#3765,.T.);
#2486=EDGE_CURVE('',#3242,#3241,#3766,.T.);
#2487=EDGE_CURVE('',#3243,#3242,#3767,.T.);
#2488=EDGE_CURVE('',#3244,#3243,#3768,.T.);
#2489=EDGE_CURVE('',#3245,#3244,#3769,.T.);
#2490=EDGE_CURVE('',#3246,#3245,#3770,.T.);
#2491=EDGE_CURVE('',#3247,#3246,#3771,.T.);
#2492=EDGE_CURVE('',#3248,#3247,#3772,.T.);
#2493=EDGE_CURVE('',#3249,#3248,#3773,.T.);
#2494=EDGE_CURVE('',#3250,#3249,#3774,.T.);
#2495=EDGE_CURVE('',#3251,#3250,#3775,.T.);
#2496=EDGE_CURVE('',#3204,#3251,#3776,.T.);
#2497=EDGE_CURVE('',#3252,#3253,#3777,.T.);
#2498=EDGE_CURVE('',#3253,#3254,#51,.T.);
#2499=EDGE_CURVE('',#3254,#3255,#3778,.T.);
#2500=EDGE_CURVE('',#3255,#3252,#52,.T.);
#2501=EDGE_CURVE('',#3198,#3210,#53,.T.);
#2502=EDGE_CURVE('',#3203,#3205,#54,.T.);
#2503=EDGE_CURVE('',#3202,#3206,#55,.T.);
#2504=EDGE_CURVE('',#3201,#3207,#56,.T.);
#2505=EDGE_CURVE('',#3200,#3208,#57,.T.);
#2506=EDGE_CURVE('',#3199,#3209,#58,.T.);
#2507=EDGE_CURVE('',#3154,#3252,#59,.T.);
#2508=EDGE_CURVE('',#3152,#3253,#60,.T.);
#2509=EDGE_CURVE('',#3153,#3254,#61,.T.);
#2510=EDGE_CURVE('',#3155,#3255,#62,.T.);
#2511=EDGE_CURVE('',#3214,#3194,#63,.F.);
#2512=EDGE_CURVE('',#3195,#3213,#64,.T.);
#2513=EDGE_CURVE('',#3218,#3190,#65,.F.);
#2514=EDGE_CURVE('',#3191,#3217,#66,.T.);
#2515=EDGE_CURVE('',#3187,#3221,#67,.T.);
#2516=EDGE_CURVE('',#3222,#3186,#68,.F.);
#2517=EDGE_CURVE('',#3183,#3225,#69,.T.);
#2518=EDGE_CURVE('',#3226,#3182,#70,.F.);
#2519=EDGE_CURVE('',#3230,#3178,#71,.F.);
#2520=EDGE_CURVE('',#3179,#3229,#72,.T.);
#2521=EDGE_CURVE('',#3234,#3174,#73,.F.);
#2522=EDGE_CURVE('',#3175,#3233,#74,.T.);
#2523=EDGE_CURVE('',#3171,#3237,#75,.T.);
#2524=EDGE_CURVE('',#3238,#3170,#76,.F.);
#2525=EDGE_CURVE('',#3242,#3166,#77,.F.);
#2526=EDGE_CURVE('',#3167,#3241,#78,.T.);
#2527=EDGE_CURVE('',#3246,#3162,#79,.F.);
#2528=EDGE_CURVE('',#3163,#3245,#80,.T.);
#2529=EDGE_CURVE('',#3250,#3158,#81,.F.);
#2530=EDGE_CURVE('',#3159,#3249,#82,.T.);
#2531=EDGE_CURVE('',#3156,#3204,#83,.T.);
#2532=EDGE_CURVE('',#3157,#3251,#84,.T.);
#2533=EDGE_CURVE('',#3160,#3248,#85,.T.);
#2534=EDGE_CURVE('',#3161,#3247,#86,.T.);
#2535=EDGE_CURVE('',#3164,#3244,#87,.T.);
#2536=EDGE_CURVE('',#3165,#3243,#88,.T.);
#2537=EDGE_CURVE('',#3168,#3240,#89,.T.);
#2538=EDGE_CURVE('',#3169,#3239,#90,.T.);
#2539=EDGE_CURVE('',#3172,#3236,#91,.T.);
#2540=EDGE_CURVE('',#3173,#3235,#92,.T.);
#2541=EDGE_CURVE('',#3176,#3232,#93,.T.);
#2542=EDGE_CURVE('',#3177,#3231,#94,.T.);
#2543=EDGE_CURVE('',#3180,#3228,#95,.T.);
#2544=EDGE_CURVE('',#3181,#3227,#96,.T.);
#2545=EDGE_CURVE('',#3184,#3224,#97,.T.);
#2546=EDGE_CURVE('',#3185,#3223,#98,.T.);
#2547=EDGE_CURVE('',#3188,#3220,#99,.T.);
#2548=EDGE_CURVE('',#3189,#3219,#100,.T.);
#2549=EDGE_CURVE('',#3192,#3216,#101,.T.);
#2550=EDGE_CURVE('',#3193,#3215,#102,.T.);
#2551=EDGE_CURVE('',#3196,#3212,#103,.T.);
#2552=EDGE_CURVE('',#3197,#3211,#104,.T.);
#3142=VERTEX_POINT('',#8538);
#3143=VERTEX_POINT('',#8539);
#3144=VERTEX_POINT('',#8541);
#3145=VERTEX_POINT('',#8543);
#3146=VERTEX_POINT('',#8547);
#3147=VERTEX_POINT('',#8548);
#3148=VERTEX_POINT('',#8550);
#3149=VERTEX_POINT('',#8552);
#3150=VERTEX_POINT('',#8556);
#3151=VERTEX_POINT('',#8558);
#3152=VERTEX_POINT('',#8561);
#3153=VERTEX_POINT('',#8562);
#3154=VERTEX_POINT('',#8564);
#3155=VERTEX_POINT('',#8566);
#3156=VERTEX_POINT('',#8569);
#3157=VERTEX_POINT('',#8571);
#3158=VERTEX_POINT('',#8573);
#3159=VERTEX_POINT('',#8575);
#3160=VERTEX_POINT('',#8577);
#3161=VERTEX_POINT('',#8579);
#3162=VERTEX_POINT('',#8581);
#3163=VERTEX_POINT('',#8583);
#3164=VERTEX_POINT('',#8585);
#3165=VERTEX_POINT('',#8587);
#3166=VERTEX_POINT('',#8589);
#3167=VERTEX_POINT('',#8591);
#3168=VERTEX_POINT('',#8593);
#3169=VERTEX_POINT('',#8595);
#3170=VERTEX_POINT('',#8597);
#3171=VERTEX_POINT('',#8599);
#3172=VERTEX_POINT('',#8601);
#3173=VERTEX_POINT('',#8603);
#3174=VERTEX_POINT('',#8605);
#3175=VERTEX_POINT('',#8607);
#3176=VERTEX_POINT('',#8609);
#3177=VERTEX_POINT('',#8611);
#3178=VERTEX_POINT('',#8613);
#3179=VERTEX_POINT('',#8615);
#3180=VERTEX_POINT('',#8617);
#3181=VERTEX_POINT('',#8619);
#3182=VERTEX_POINT('',#8621);
#3183=VERTEX_POINT('',#8623);
#3184=VERTEX_POINT('',#8625);
#3185=VERTEX_POINT('',#8627);
#3186=VERTEX_POINT('',#8629);
#3187=VERTEX_POINT('',#8631);
#3188=VERTEX_POINT('',#8633);
#3189=VERTEX_POINT('',#8635);
#3190=VERTEX_POINT('',#8637);
#3191=VERTEX_POINT('',#8639);
#3192=VERTEX_POINT('',#8641);
#3193=VERTEX_POINT('',#8643);
#3194=VERTEX_POINT('',#8645);
#3195=VERTEX_POINT('',#8647);
#3196=VERTEX_POINT('',#8649);
#3197=VERTEX_POINT('',#8651);
#3198=VERTEX_POINT('',#8654);
#3199=VERTEX_POINT('',#8656);
#3200=VERTEX_POINT('',#8658);
#3201=VERTEX_POINT('',#8660);
#3202=VERTEX_POINT('',#8662);
#3203=VERTEX_POINT('',#8664);
#3204=VERTEX_POINT('',#8668);
#3205=VERTEX_POINT('',#8670);
#3206=VERTEX_POINT('',#8672);
#3207=VERTEX_POINT('',#8674);
#3208=VERTEX_POINT('',#8676);
#3209=VERTEX_POINT('',#8678);
#3210=VERTEX_POINT('',#8680);
#3211=VERTEX_POINT('',#8683);
#3212=VERTEX_POINT('',#8685);
#3213=VERTEX_POINT('',#8687);
#3214=VERTEX_POINT('',#8689);
#3215=VERTEX_POINT('',#8691);
#3216=VERTEX_POINT('',#8693);
#3217=VERTEX_POINT('',#8695);
#3218=VERTEX_POINT('',#8697);
#3219=VERTEX_POINT('',#8699);
#3220=VERTEX_POINT('',#8701);
#3221=VERTEX_POINT('',#8703);
#3222=VERTEX_POINT('',#8705);
#3223=VERTEX_POINT('',#8707);
#3224=VERTEX_POINT('',#8709);
#3225=VERTEX_POINT('',#8711);
#3226=VERTEX_POINT('',#8713);
#3227=VERTEX_POINT('',#8715);
#3228=VERTEX_POINT('',#8717);
#3229=VERTEX_POINT('',#8719);
#3230=VERTEX_POINT('',#8721);
#3231=VERTEX_POINT('',#8723);
#3232=VERTEX_POINT('',#8725);
#3233=VERTEX_POINT('',#8727);
#3234=VERTEX_POINT('',#8729);
#3235=VERTEX_POINT('',#8731);
#3236=VERTEX_POINT('',#8733);
#3237=VERTEX_POINT('',#8735);
#3238=VERTEX_POINT('',#8737);
#3239=VERTEX_POINT('',#8739);
#3240=VERTEX_POINT('',#8741);
#3241=VERTEX_POINT('',#8743);
#3242=VERTEX_POINT('',#8745);
#3243=VERTEX_POINT('',#8747);
#3244=VERTEX_POINT('',#8749);
#3245=VERTEX_POINT('',#8751);
#3246=VERTEX_POINT('',#8753);
#3247=VERTEX_POINT('',#8755);
#3248=VERTEX_POINT('',#8757);
#3249=VERTEX_POINT('',#8759);
#3250=VERTEX_POINT('',#8761);
#3251=VERTEX_POINT('',#8763);
#3252=VERTEX_POINT('',#8766);
#3253=VERTEX_POINT('',#8767);
#3254=VERTEX_POINT('',#8769);
#3255=VERTEX_POINT('',#8771);
#3675=CIRCLE('',#5759,0.0125);
#3676=CIRCLE('',#5760,0.0125);
#3677=CIRCLE('',#5762,0.0125);
#3678=CIRCLE('',#5763,0.0125);
#3679=CIRCLE('',#5765,0.0015);
#3680=CIRCLE('',#5766,0.0015);
#3681=CIRCLE('',#5768,0.0015);
#3682=CIRCLE('',#5769,0.0015);
#3683=CIRCLE('',#5770,0.0048);
#3684=CIRCLE('',#5771,0.011374);
#3685=CIRCLE('',#5772,0.0048);
#3686=CIRCLE('',#5773,0.0125);
#3687=CIRCLE('',#5774,0.0048);
#3688=CIRCLE('',#5775,0.011374);
#3689=CIRCLE('',#5776,0.0048);
#3690=CIRCLE('',#5777,0.0125);
#3691=CIRCLE('',#5778,0.0048);
#3692=CIRCLE('',#5779,0.011374);
#3693=CIRCLE('',#5780,0.0048);
#3694=CIRCLE('',#5781,0.0125);
#3695=CIRCLE('',#5782,0.0048);
#3696=CIRCLE('',#5783,0.011374);
#3697=CIRCLE('',#5784,0.0048);
#3698=CIRCLE('',#5785,0.0125);
#3699=CIRCLE('',#5786,0.0048);
#3700=CIRCLE('',#5787,0.011374);
#3701=CIRCLE('',#5788,0.0048);
#3702=CIRCLE('',#5789,0.0125);
#3703=CIRCLE('',#5790,0.0048);
#3704=CIRCLE('',#5791,0.011374);
#3705=CIRCLE('',#5792,0.0048);
#3706=CIRCLE('',#5793,0.0125);
#3707=CIRCLE('',#5794,0.0048);
#3708=CIRCLE('',#5795,0.011374);
#3709=CIRCLE('',#5796,0.0048);
#3710=CIRCLE('',#5797,0.0125);
#3711=CIRCLE('',#5798,0.0048);
#3712=CIRCLE('',#5799,0.011374);
#3713=CIRCLE('',#5800,0.0048);
#3714=CIRCLE('',#5801,0.0125);
#3715=CIRCLE('',#5802,0.0048);
#3716=CIRCLE('',#5803,0.011374);
#3717=CIRCLE('',#5804,0.0048);
#3718=CIRCLE('',#5805,0.0125);
#3719=CIRCLE('',#5806,0.0048);
#3720=CIRCLE('',#5807,0.011374);
#3721=CIRCLE('',#5808,0.0048);
#3722=CIRCLE('',#5809,0.0125);
#3723=CIRCLE('',#5810,0.0048);
#3724=CIRCLE('',#5811,0.011374);
#3725=CIRCLE('',#5812,0.0048);
#3726=CIRCLE('',#5813,0.015);
#3727=CIRCLE('',#5814,0.00499999999999989);
#3728=CIRCLE('',#5815,0.005);
#3729=CIRCLE('',#5816,0.0354217830972575);
#3730=CIRCLE('',#5818,0.0048);
#3731=CIRCLE('',#5819,0.0354217830972575);
#3732=CIRCLE('',#5820,0.005);
#3733=CIRCLE('',#5821,0.00499999999999989);
#3734=CIRCLE('',#5822,0.015);
#3735=CIRCLE('',#5823,0.0048);
#3736=CIRCLE('',#5824,0.011374);
#3737=CIRCLE('',#5825,0.0048);
#3738=CIRCLE('',#5826,0.0125);
#3739=CIRCLE('',#5827,0.0048);
#3740=CIRCLE('',#5828,0.011374);
#3741=CIRCLE('',#5829,0.0048);
#3742=CIRCLE('',#5830,0.0125);
#3743=CIRCLE('',#5831,0.0048);
#3744=CIRCLE('',#5832,0.011374);
#3745=CIRCLE('',#5833,0.0048);
#3746=CIRCLE('',#5834,0.0125);
#3747=CIRCLE('',#5835,0.0048);
#3748=CIRCLE('',#5836,0.011374);
#3749=CIRCLE('',#5837,0.0048);
#3750=CIRCLE('',#5838,0.0125);
#3751=CIRCLE('',#5839,0.0048);
#3752=CIRCLE('',#5840,0.011374);
#3753=CIRCLE('',#5841,0.0048);
#3754=CIRCLE('',#5842,0.0125);
#3755=CIRCLE('',#5843,0.0048);
#3756=CIRCLE('',#5844,0.011374);
#3757=CIRCLE('',#5845,0.0048);
#3758=CIRCLE('',#5846,0.0125);
#3759=CIRCLE('',#5847,0.0048);
#3760=CIRCLE('',#5848,0.011374);
#3761=CIRCLE('',#5849,0.0048);
#3762=CIRCLE('',#5850,0.0125);
#3763=CIRCLE('',#5851,0.0048);
#3764=CIRCLE('',#5852,0.011374);
#3765=CIRCLE('',#5853,0.0048);
#3766=CIRCLE('',#5854,0.0125);
#3767=CIRCLE('',#5855,0.0048);
#3768=CIRCLE('',#5856,0.011374);
#3769=CIRCLE('',#5857,0.0048);
#3770=CIRCLE('',#5858,0.0125);
#3771=CIRCLE('',#5859,0.0048);
#3772=CIRCLE('',#5860,0.011374);
#3773=CIRCLE('',#5861,0.0048);
#3774=CIRCLE('',#5862,0.0125);
#3775=CIRCLE('',#5863,0.0048);
#3776=CIRCLE('',#5864,0.011374);
#3777=CIRCLE('',#5865,0.0015);
#3778=CIRCLE('',#5866,0.0015);
#4157=EDGE_LOOP('',(#892,#893,#894,#895));
#4158=EDGE_LOOP('',(#896,#897,#898,#899));
#4159=EDGE_LOOP('',(#900));
#4160=EDGE_LOOP('',(#901));
#4161=EDGE_LOOP('',(#902));
#4162=EDGE_LOOP('',(#903,#904,#905,#906));
#4163=EDGE_LOOP('',(#907,#908,#909,#910,#911,#912,#913,#914,#915,#916,#917,
#918,#919,#920,#921,#922,#923,#924,#925,#926,#927,#928,#929,#930,#931,#932,
#933,#934,#935,#936,#937,#938,#939,#940,#941,#942,#943,#944,#945,#946,#947,
#948,#949,#950,#951,#952,#953,#954,#955,#956,#957,#958));
#4164=EDGE_LOOP('',(#959));
#4165=EDGE_LOOP('',(#960,#961,#962,#963,#964,#965,#966,#967,#968,#969,#970,
#971,#972,#973,#974,#975,#976,#977,#978,#979,#980,#981,#982,#983,#984,#985,
#986,#987,#988,#989,#990,#991,#992,#993,#994,#995,#996,#997,#998,#999,#1000,
#1001,#1002,#1003,#1004,#1005,#1006,#1007,#1008,#1009,#1010,#1011));
#4166=EDGE_LOOP('',(#1012,#1013,#1014,#1015));
#4167=EDGE_LOOP('',(#1016,#1017,#1018,#1019));
#4168=EDGE_LOOP('',(#1020,#1021,#1022,#1023));
#4169=EDGE_LOOP('',(#1024,#1025,#1026,#1027));
#4170=EDGE_LOOP('',(#1028,#1029,#1030,#1031));
#4171=EDGE_LOOP('',(#1032,#1033,#1034,#1035));
#4172=EDGE_LOOP('',(#1036,#1037,#1038,#1039));
#4173=EDGE_LOOP('',(#1040,#1041,#1042,#1043));
#4174=EDGE_LOOP('',(#1044,#1045,#1046,#1047));
#4175=EDGE_LOOP('',(#1048,#1049,#1050,#1051));
#4176=EDGE_LOOP('',(#1052,#1053,#1054,#1055));
#4177=EDGE_LOOP('',(#1056,#1057,#1058,#1059));
#4178=EDGE_LOOP('',(#1060,#1061,#1062,#1063));
#4179=EDGE_LOOP('',(#1064,#1065,#1066,#1067));
#4180=EDGE_LOOP('',(#1068,#1069,#1070,#1071));
#4181=EDGE_LOOP('',(#1072,#1073,#1074,#1075));
#4182=EDGE_LOOP('',(#1076,#1077,#1078,#1079));
#4183=EDGE_LOOP('',(#1080,#1081,#1082,#1083));
#4184=EDGE_LOOP('',(#1084,#1085,#1086,#1087));
#4185=EDGE_LOOP('',(#1088,#1089,#1090,#1091));
#4186=EDGE_LOOP('',(#1092,#1093,#1094,#1095));
#4187=EDGE_LOOP('',(#1096,#1097,#1098,#1099));
#4188=EDGE_LOOP('',(#1100,#1101,#1102,#1103));
#4189=EDGE_LOOP('',(#1104,#1105,#1106,#1107));
#4190=EDGE_LOOP('',(#1108,#1109,#1110,#1111));
#4191=EDGE_LOOP('',(#1112,#1113,#1114,#1115));
#4192=EDGE_LOOP('',(#1116,#1117,#1118,#1119));
#4193=EDGE_LOOP('',(#1120,#1121,#1122,#1123));
#4194=EDGE_LOOP('',(#1124,#1125,#1126,#1127));
#4195=EDGE_LOOP('',(#1128,#1129,#1130,#1131));
#4196=EDGE_LOOP('',(#1132,#1133,#1134,#1135));
#4197=EDGE_LOOP('',(#1136,#1137,#1138,#1139));
#4198=EDGE_LOOP('',(#1140,#1141,#1142,#1143));
#4199=EDGE_LOOP('',(#1144,#1145,#1146,#1147));
#4200=EDGE_LOOP('',(#1148,#1149,#1150,#1151));
#4201=EDGE_LOOP('',(#1152,#1153,#1154,#1155));
#4202=EDGE_LOOP('',(#1156,#1157,#1158,#1159));
#4203=EDGE_LOOP('',(#1160,#1161,#1162,#1163));
#4204=EDGE_LOOP('',(#1164,#1165,#1166,#1167));
#4205=EDGE_LOOP('',(#1168,#1169,#1170,#1171));
#4206=EDGE_LOOP('',(#1172,#1173,#1174,#1175));
#4207=EDGE_LOOP('',(#1176,#1177,#1178,#1179));
#4208=EDGE_LOOP('',(#1180,#1181,#1182,#1183));
#4209=EDGE_LOOP('',(#1184,#1185,#1186,#1187));
#4210=EDGE_LOOP('',(#1188,#1189,#1190,#1191));
#4211=EDGE_LOOP('',(#1192,#1193,#1194,#1195));
#4212=EDGE_LOOP('',(#1196,#1197,#1198,#1199));
#4213=EDGE_LOOP('',(#1200,#1201,#1202,#1203));
#4214=EDGE_LOOP('',(#1204,#1205,#1206,#1207));
#4215=EDGE_LOOP('',(#1208,#1209,#1210,#1211));
#4216=EDGE_LOOP('',(#1212,#1213,#1214,#1215));
#4217=EDGE_LOOP('',(#1216,#1217,#1218,#1219));
#4218=EDGE_LOOP('',(#1220,#1221,#1222,#1223));
#4219=EDGE_LOOP('',(#1224,#1225,#1226,#1227));
#4220=EDGE_LOOP('',(#1228,#1229,#1230,#1231));
#4605=FACE_BOUND('',#4157,.T.);
#4606=FACE_BOUND('',#4158,.T.);
#4607=FACE_BOUND('',#4159,.T.);
#4608=FACE_BOUND('',#4160,.T.);
#4609=FACE_BOUND('',#4161,.T.);
#4610=FACE_BOUND('',#4162,.T.);
#4611=FACE_BOUND('',#4163,.T.);
#4612=FACE_BOUND('',#4164,.T.);
#4613=FACE_BOUND('',#4165,.T.);
#4614=FACE_BOUND('',#4166,.T.);
#4615=FACE_BOUND('',#4167,.T.);
#4616=FACE_BOUND('',#4168,.T.);
#4617=FACE_BOUND('',#4169,.T.);
#4618=FACE_BOUND('',#4170,.T.);
#4619=FACE_BOUND('',#4171,.T.);
#4620=FACE_BOUND('',#4172,.T.);
#4621=FACE_BOUND('',#4173,.T.);
#4622=FACE_BOUND('',#4174,.T.);
#4623=FACE_BOUND('',#4175,.T.);
#4624=FACE_BOUND('',#4176,.T.);
#4625=FACE_BOUND('',#4177,.T.);
#4626=FACE_BOUND('',#4178,.T.);
#4627=FACE_BOUND('',#4179,.T.);
#4628=FACE_BOUND('',#4180,.T.);
#4629=FACE_BOUND('',#4181,.T.);
#4630=FACE_BOUND('',#4182,.T.);
#4631=FACE_BOUND('',#4183,.T.);
#4632=FACE_BOUND('',#4184,.T.);
#4633=FACE_BOUND('',#4185,.T.);
#4634=FACE_BOUND('',#4186,.T.);
#4635=FACE_BOUND('',#4187,.T.);
#4636=FACE_BOUND('',#4188,.T.);
#4637=FACE_BOUND('',#4189,.T.);
#4638=FACE_BOUND('',#4190,.T.);
#4639=FACE_BOUND('',#4191,.T.);
#4640=FACE_BOUND('',#4192,.T.);
#4641=FACE_BOUND('',#4193,.T.);
#4642=FACE_BOUND('',#4194,.T.);
#4643=FACE_BOUND('',#4195,.T.);
#4644=FACE_BOUND('',#4196,.T.);
#4645=FACE_BOUND('',#4197,.T.);
#4646=FACE_BOUND('',#4198,.T.);
#4647=FACE_BOUND('',#4199,.T.);
#4648=FACE_BOUND('',#4200,.T.);
#4649=FACE_BOUND('',#4201,.T.);
#4650=FACE_BOUND('',#4202,.T.);
#4651=FACE_BOUND('',#4203,.T.);
#4652=FACE_BOUND('',#4204,.T.);
#4653=FACE_BOUND('',#4205,.T.);
#4654=FACE_BOUND('',#4206,.T.);
#4655=FACE_BOUND('',#4207,.T.);
#4656=FACE_BOUND('',#4208,.T.);
#4657=FACE_BOUND('',#4209,.T.);
#4658=FACE_BOUND('',#4210,.T.);
#4659=FACE_BOUND('',#4211,.T.);
#4660=FACE_BOUND('',#4212,.T.);
#4661=FACE_BOUND('',#4213,.T.);
#4662=FACE_BOUND('',#4214,.T.);
#4663=FACE_BOUND('',#4215,.T.);
#4664=FACE_BOUND('',#4216,.T.);
#4665=FACE_BOUND('',#4217,.T.);
#4666=FACE_BOUND('',#4218,.T.);
#4667=FACE_BOUND('',#4219,.T.);
#4668=FACE_BOUND('',#4220,.T.);
#5012=CYLINDRICAL_SURFACE('',#5758,0.0125);
#5013=CYLINDRICAL_SURFACE('',#5761,0.0125);
#5014=CYLINDRICAL_SURFACE('',#5764,0.0015);
#5015=CYLINDRICAL_SURFACE('',#5868,0.0354217830972575);
#5016=CYLINDRICAL_SURFACE('',#5869,0.005);
#5017=CYLINDRICAL_SURFACE('',#5871,0.00499999999999989);
#5018=CYLINDRICAL_SURFACE('',#5873,0.015);
#5019=CYLINDRICAL_SURFACE('',#5874,0.0015);
#5020=CYLINDRICAL_SURFACE('',#5876,0.0015);
#5021=CYLINDRICAL_SURFACE('',#5878,0.0125);
#5022=CYLINDRICAL_SURFACE('',#5879,0.0125);
#5023=CYLINDRICAL_SURFACE('',#5880,0.0125);
#5024=CYLINDRICAL_SURFACE('',#5881,0.0125);
#5025=CYLINDRICAL_SURFACE('',#5882,0.0125);
#5026=CYLINDRICAL_SURFACE('',#5883,0.0125);
#5027=CYLINDRICAL_SURFACE('',#5884,0.0125);
#5028=CYLINDRICAL_SURFACE('',#5885,0.0125);
#5029=CYLINDRICAL_SURFACE('',#5886,0.0125);
#5030=CYLINDRICAL_SURFACE('',#5887,0.0125);
#5031=CYLINDRICAL_SURFACE('',#5888,0.0048);
#5032=CYLINDRICAL_SURFACE('',#5889,0.011374);
#5033=CYLINDRICAL_SURFACE('',#5890,0.0048);
#5034=CYLINDRICAL_SURFACE('',#5891,0.0048);
#5035=CYLINDRICAL_SURFACE('',#5892,0.011374);
#5036=CYLINDRICAL_SURFACE('',#5893,0.0048);
#5037=CYLINDRICAL_SURFACE('',#5894,0.0048);
#5038=CYLINDRICAL_SURFACE('',#5895,0.011374);
#5039=CYLINDRICAL_SURFACE('',#5896,0.0048);
#5040=CYLINDRICAL_SURFACE('',#5897,0.0048);
#5041=CYLINDRICAL_SURFACE('',#5898,0.011374);
#5042=CYLINDRICAL_SURFACE('',#5899,0.0048);
#5043=CYLINDRICAL_SURFACE('',#5900,0.0048);
#5044=CYLINDRICAL_SURFACE('',#5901,0.011374);
#5045=CYLINDRICAL_SURFACE('',#5902,0.0048);
#5046=CYLINDRICAL_SURFACE('',#5903,0.0048);
#5047=CYLINDRICAL_SURFACE('',#5904,0.011374);
#5048=CYLINDRICAL_SURFACE('',#5905,0.0048);
#5049=CYLINDRICAL_SURFACE('',#5906,0.0048);
#5050=CYLINDRICAL_SURFACE('',#5907,0.011374);
#5051=CYLINDRICAL_SURFACE('',#5908,0.0048);
#5052=CYLINDRICAL_SURFACE('',#5909,0.0048);
#5053=CYLINDRICAL_SURFACE('',#5910,0.011374);
#5054=CYLINDRICAL_SURFACE('',#5911,0.0048);
#5055=CYLINDRICAL_SURFACE('',#5912,0.0048);
#5056=CYLINDRICAL_SURFACE('',#5913,0.011374);
#5057=CYLINDRICAL_SURFACE('',#5914,0.0048);
#5058=CYLINDRICAL_SURFACE('',#5915,0.0048);
#5059=CYLINDRICAL_SURFACE('',#5916,0.011374);
#5060=CYLINDRICAL_SURFACE('',#5917,0.0048);
#5061=CYLINDRICAL_SURFACE('',#5918,0.0048);
#5062=CYLINDRICAL_SURFACE('',#5919,0.011374);
#5063=CYLINDRICAL_SURFACE('',#5920,0.0048);
#5238=ADVANCED_FACE('',(#4605),#5012,.T.);
#5239=ADVANCED_FACE('',(#4606),#5013,.T.);
#5240=ADVANCED_FACE('',(#4607,#4608),#5014,.F.);
#5241=ADVANCED_FACE('',(#4609,#4610,#4611),#710,.T.);
#5242=ADVANCED_FACE('',(#4612,#4613,#4614),#711,.F.);
#5243=ADVANCED_FACE('',(#4615),#712,.F.);
#5244=ADVANCED_FACE('',(#4616),#5015,.F.);
#5245=ADVANCED_FACE('',(#4617),#5016,.F.);
#5246=ADVANCED_FACE('',(#4618),#713,.F.);
#5247=ADVANCED_FACE('',(#4619),#5017,.T.);
#5248=ADVANCED_FACE('',(#4620),#714,.F.);
#5249=ADVANCED_FACE('',(#4621),#5018,.T.);
#5250=ADVANCED_FACE('',(#4622),#5019,.F.);
#5251=ADVANCED_FACE('',(#4623),#715,.T.);
#5252=ADVANCED_FACE('',(#4624),#5020,.F.);
#5253=ADVANCED_FACE('',(#4625),#716,.T.);
#5254=ADVANCED_FACE('',(#4626),#5021,.T.);
#5255=ADVANCED_FACE('',(#4627),#5022,.T.);
#5256=ADVANCED_FACE('',(#4628),#5023,.T.);
#5257=ADVANCED_FACE('',(#4629),#5024,.T.);
#5258=ADVANCED_FACE('',(#4630),#5025,.T.);
#5259=ADVANCED_FACE('',(#4631),#5026,.T.);
#5260=ADVANCED_FACE('',(#4632),#5027,.T.);
#5261=ADVANCED_FACE('',(#4633),#5028,.T.);
#5262=ADVANCED_FACE('',(#4634),#5029,.T.);
#5263=ADVANCED_FACE('',(#4635),#5030,.T.);
#5264=ADVANCED_FACE('',(#4636),#5031,.T.);
#5265=ADVANCED_FACE('',(#4637),#5032,.T.);
#5266=ADVANCED_FACE('',(#4638),#5033,.T.);
#5267=ADVANCED_FACE('',(#4639),#5034,.T.);
#5268=ADVANCED_FACE('',(#4640),#5035,.T.);
#5269=ADVANCED_FACE('',(#4641),#5036,.T.);
#5270=ADVANCED_FACE('',(#4642),#5037,.T.);
#5271=ADVANCED_FACE('',(#4643),#5038,.T.);
#5272=ADVANCED_FACE('',(#4644),#5039,.T.);
#5273=ADVANCED_FACE('',(#4645),#5040,.T.);
#5274=ADVANCED_FACE('',(#4646),#5041,.T.);
#5275=ADVANCED_FACE('',(#4647),#5042,.T.);
#5276=ADVANCED_FACE('',(#4648),#5043,.T.);
#5277=ADVANCED_FACE('',(#4649),#5044,.T.);
#5278=ADVANCED_FACE('',(#4650),#5045,.T.);
#5279=ADVANCED_FACE('',(#4651),#5046,.T.);
#5280=ADVANCED_FACE('',(#4652),#5047,.T.);
#5281=ADVANCED_FACE('',(#4653),#5048,.T.);
#5282=ADVANCED_FACE('',(#4654),#5049,.T.);
#5283=ADVANCED_FACE('',(#4655),#5050,.T.);
#5284=ADVANCED_FACE('',(#4656),#5051,.T.);
#5285=ADVANCED_FACE('',(#4657),#5052,.T.);
#5286=ADVANCED_FACE('',(#4658),#5053,.T.);
#5287=ADVANCED_FACE('',(#4659),#5054,.T.);
#5288=ADVANCED_FACE('',(#4660),#5055,.T.);
#5289=ADVANCED_FACE('',(#4661),#5056,.T.);
#5290=ADVANCED_FACE('',(#4662),#5057,.T.);
#5291=ADVANCED_FACE('',(#4663),#5058,.T.);
#5292=ADVANCED_FACE('',(#4664),#5059,.T.);
#5293=ADVANCED_FACE('',(#4665),#5060,.T.);
#5294=ADVANCED_FACE('',(#4666),#5061,.T.);
#5295=ADVANCED_FACE('',(#4667),#5062,.T.);
#5296=ADVANCED_FACE('',(#4668),#5063,.T.);
#5541=CLOSED_SHELL('',(#5238,#5239,#5240,#5241,#5242,#5243,#5244,#5245,
#5246,#5247,#5248,#5249,#5250,#5251,#5252,#5253,#5254,#5255,#5256,#5257,
#5258,#5259,#5260,#5261,#5262,#5263,#5264,#5265,#5266,#5267,#5268,#5269,
#5270,#5271,#5272,#5273,#5274,#5275,#5276,#5277,#5278,#5279,#5280,#5281,
#5282,#5283,#5284,#5285,#5286,#5287,#5288,#5289,#5290,#5291,#5292,#5293,
#5294,#5295,#5296));
#5555=STYLED_ITEM('',(#5569),#5660);
#5569=PRESENTATION_STYLE_ASSIGNMENT((#5583));
#5583=SURFACE_STYLE_USAGE(.BOTH.,#5597);
#5597=SURFACE_SIDE_STYLE('',(#5611));
#5611=SURFACE_STYLE_FILL_AREA(#5625);
#5625=FILL_AREA_STYLE('',(#5639));
#5639=FILL_AREA_STYLE_COLOUR('',#5653);
#5653=COLOUR_RGB('', 0.40784314, 0.44705882, 0.49803922);
#5660=MANIFOLD_SOLID_BREP('Part 1',#5541);
#5675=SHAPE_DEFINITION_REPRESENTATION(#10183,#5691);
#5691=SHAPE_REPRESENTATION('Part 1',(#5704),#10145);
#5704=AXIS2_PLACEMENT_3D('',#8391,#6505,#6506);
#5758=AXIS2_PLACEMENT_3D('',#8536,#6617,#6618);
#5759=AXIS2_PLACEMENT_3D('',#8537,#6619,#6620);
#5760=AXIS2_PLACEMENT_3D('',#8542,#6622,#6623);
#5761=AXIS2_PLACEMENT_3D('',#8545,#6625,#6626);
#5762=AXIS2_PLACEMENT_3D('',#8546,#6627,#6628);
#5763=AXIS2_PLACEMENT_3D('',#8551,#6630,#6631);
#5764=AXIS2_PLACEMENT_3D('',#8554,#6633,#6634);
#5765=AXIS2_PLACEMENT_3D('',#8555,#6635,#6636);
#5766=AXIS2_PLACEMENT_3D('',#8557,#6637,#6638);
#5767=AXIS2_PLACEMENT_3D('',#8559,#6639,#6640);
#5768=AXIS2_PLACEMENT_3D('',#8563,#6642,#6643);
#5769=AXIS2_PLACEMENT_3D('',#8567,#6645,#6646);
#5770=AXIS2_PLACEMENT_3D('',#8568,#6647,#6648);
#5771=AXIS2_PLACEMENT_3D('',#8570,#6649,#6650);
#5772=AXIS2_PLACEMENT_3D('',#8572,#6651,#6652);
#5773=AXIS2_PLACEMENT_3D('',#8574,#6653,#6654);
#5774=AXIS2_PLACEMENT_3D('',#8576,#6655,#6656);
#5775=AXIS2_PLACEMENT_3D('',#8578,#6657,#6658);
#5776=AXIS2_PLACEMENT_3D('',#8580,#6659,#6660);
#5777=AXIS2_PLACEMENT_3D('',#8582,#6661,#6662);
#5778=AXIS2_PLACEMENT_3D('',#8584,#6663,#6664);
#5779=AXIS2_PLACEMENT_3D('',#8586,#6665,#6666);
#5780=AXIS2_PLACEMENT_3D('',#8588,#6667,#6668);
#5781=AXIS2_PLACEMENT_3D('',#8590,#6669,#6670);
#5782=AXIS2_PLACEMENT_3D('',#8592,#6671,#6672);
#5783=AXIS2_PLACEMENT_3D('',#8594,#6673,#6674);
#5784=AXIS2_PLACEMENT_3D('',#8596,#6675,#6676);
#5785=AXIS2_PLACEMENT_3D('',#8598,#6677,#6678);
#5786=AXIS2_PLACEMENT_3D('',#8600,#6679,#6680);
#5787=AXIS2_PLACEMENT_3D('',#8602,#6681,#6682);
#5788=AXIS2_PLACEMENT_3D('',#8604,#6683,#6684);
#5789=AXIS2_PLACEMENT_3D('',#8606,#6685,#6686);
#5790=AXIS2_PLACEMENT_3D('',#8608,#6687,#6688);
#5791=AXIS2_PLACEMENT_3D('',#8610,#6689,#6690);
#5792=AXIS2_PLACEMENT_3D('',#8612,#6691,#6692);
#5793=AXIS2_PLACEMENT_3D('',#8614,#6693,#6694);
#5794=AXIS2_PLACEMENT_3D('',#8616,#6695,#6696);
#5795=AXIS2_PLACEMENT_3D('',#8618,#6697,#6698);
#5796=AXIS2_PLACEMENT_3D('',#8620,#6699,#6700);
#5797=AXIS2_PLACEMENT_3D('',#8622,#6701,#6702);
#5798=AXIS2_PLACEMENT_3D('',#8624,#6703,#6704);
#5799=AXIS2_PLACEMENT_3D('',#8626,#6705,#6706);
#5800=AXIS2_PLACEMENT_3D('',#8628,#6707,#6708);
#5801=AXIS2_PLACEMENT_3D('',#8630,#6709,#6710);
#5802=AXIS2_PLACEMENT_3D('',#8632,#6711,#6712);
#5803=AXIS2_PLACEMENT_3D('',#8634,#6713,#6714);
#5804=AXIS2_PLACEMENT_3D('',#8636,#6715,#6716);
#5805=AXIS2_PLACEMENT_3D('',#8638,#6717,#6718);
#5806=AXIS2_PLACEMENT_3D('',#8640,#6719,#6720);
#5807=AXIS2_PLACEMENT_3D('',#8642,#6721,#6722);
#5808=AXIS2_PLACEMENT_3D('',#8644,#6723,#6724);
#5809=AXIS2_PLACEMENT_3D('',#8646,#6725,#6726);
#5810=AXIS2_PLACEMENT_3D('',#8648,#6727,#6728);
#5811=AXIS2_PLACEMENT_3D('',#8650,#6729,#6730);
#5812=AXIS2_PLACEMENT_3D('',#8652,#6731,#6732);
#5813=AXIS2_PLACEMENT_3D('',#8655,#6734,#6735);
#5814=AXIS2_PLACEMENT_3D('',#8659,#6737,#6738);
#5815=AXIS2_PLACEMENT_3D('',#8663,#6740,#6741);
#5816=AXIS2_PLACEMENT_3D('',#8665,#6742,#6743);
#5817=AXIS2_PLACEMENT_3D('',#8666,#6744,#6745);
#5818=AXIS2_PLACEMENT_3D('',#8667,#6746,#6747);
#5819=AXIS2_PLACEMENT_3D('',#8669,#6748,#6749);
#5820=AXIS2_PLACEMENT_3D('',#8671,#6750,#6751);
#5821=AXIS2_PLACEMENT_3D('',#8675,#6753,#6754);
#5822=AXIS2_PLACEMENT_3D('',#8679,#6756,#6757);
#5823=AXIS2_PLACEMENT_3D('',#8682,#6759,#6760);
#5824=AXIS2_PLACEMENT_3D('',#8684,#6761,#6762);
#5825=AXIS2_PLACEMENT_3D('',#8686,#6763,#6764);
#5826=AXIS2_PLACEMENT_3D('',#8688,#6765,#6766);
#5827=AXIS2_PLACEMENT_3D('',#8690,#6767,#6768);
#5828=AXIS2_PLACEMENT_3D('',#8692,#6769,#6770);
#5829=AXIS2_PLACEMENT_3D('',#8694,#6771,#6772);
#5830=AXIS2_PLACEMENT_3D('',#8696,#6773,#6774);
#5831=AXIS2_PLACEMENT_3D('',#8698,#6775,#6776);
#5832=AXIS2_PLACEMENT_3D('',#8700,#6777,#6778);
#5833=AXIS2_PLACEMENT_3D('',#8702,#6779,#6780);
#5834=AXIS2_PLACEMENT_3D('',#8704,#6781,#6782);
#5835=AXIS2_PLACEMENT_3D('',#8706,#6783,#6784);
#5836=AXIS2_PLACEMENT_3D('',#8708,#6785,#6786);
#5837=AXIS2_PLACEMENT_3D('',#8710,#6787,#6788);
#5838=AXIS2_PLACEMENT_3D('',#8712,#6789,#6790);
#5839=AXIS2_PLACEMENT_3D('',#8714,#6791,#6792);
#5840=AXIS2_PLACEMENT_3D('',#8716,#6793,#6794);
#5841=AXIS2_PLACEMENT_3D('',#8718,#6795,#6796);
#5842=AXIS2_PLACEMENT_3D('',#8720,#6797,#6798);
#5843=AXIS2_PLACEMENT_3D('',#8722,#6799,#6800);
#5844=AXIS2_PLACEMENT_3D('',#8724,#6801,#6802);
#5845=AXIS2_PLACEMENT_3D('',#8726,#6803,#6804);
#5846=AXIS2_PLACEMENT_3D('',#8728,#6805,#6806);
#5847=AXIS2_PLACEMENT_3D('',#8730,#6807,#6808);
#5848=AXIS2_PLACEMENT_3D('',#8732,#6809,#6810);
#5849=AXIS2_PLACEMENT_3D('',#8734,#6811,#6812);
#5850=AXIS2_PLACEMENT_3D('',#8736,#6813,#6814);
#5851=AXIS2_PLACEMENT_3D('',#8738,#6815,#6816);
#5852=AXIS2_PLACEMENT_3D('',#8740,#6817,#6818);
#5853=AXIS2_PLACEMENT_3D('',#8742,#6819,#6820);
#5854=AXIS2_PLACEMENT_3D('',#8744,#6821,#6822);
#5855=AXIS2_PLACEMENT_3D('',#8746,#6823,#6824);
#5856=AXIS2_PLACEMENT_3D('',#8748,#6825,#6826);
#5857=AXIS2_PLACEMENT_3D('',#8750,#6827,#6828);
#5858=AXIS2_PLACEMENT_3D('',#8752,#6829,#6830);
#5859=AXIS2_PLACEMENT_3D('',#8754,#6831,#6832);
#5860=AXIS2_PLACEMENT_3D('',#8756,#6833,#6834);
#5861=AXIS2_PLACEMENT_3D('',#8758,#6835,#6836);
#5862=AXIS2_PLACEMENT_3D('',#8760,#6837,#6838);
#5863=AXIS2_PLACEMENT_3D('',#8762,#6839,#6840);
#5864=AXIS2_PLACEMENT_3D('',#8764,#6841,#6842);
#5865=AXIS2_PLACEMENT_3D('',#8765,#6843,#6844);
#5866=AXIS2_PLACEMENT_3D('',#8770,#6846,#6847);
#5867=AXIS2_PLACEMENT_3D('',#8773,#6849,#6850);
#5868=AXIS2_PLACEMENT_3D('',#8775,#6852,#6853);
#5869=AXIS2_PLACEMENT_3D('',#8777,#6855,#6856);
#5870=AXIS2_PLACEMENT_3D('',#8779,#6858,#6859);
#5871=AXIS2_PLACEMENT_3D('',#8781,#6861,#6862);
#5872=AXIS2_PLACEMENT_3D('',#8783,#6864,#6865);
#5873=AXIS2_PLACEMENT_3D('',#8785,#6867,#6868);
#5874=AXIS2_PLACEMENT_3D('',#8786,#6869,#6870);
#5875=AXIS2_PLACEMENT_3D('',#8789,#6873,#6874);
#5876=AXIS2_PLACEMENT_3D('',#8791,#6876,#6877);
#5877=AXIS2_PLACEMENT_3D('',#8793,#6879,#6880);
#5878=AXIS2_PLACEMENT_3D('',#8794,#6881,#6882);
#5879=AXIS2_PLACEMENT_3D('',#8797,#6885,#6886);
#5880=AXIS2_PLACEMENT_3D('',#8800,#6889,#6890);
#5881=AXIS2_PLACEMENT_3D('',#8803,#6893,#6894);
#5882=AXIS2_PLACEMENT_3D('',#8806,#6897,#6898);
#5883=AXIS2_PLACEMENT_3D('',#8809,#6901,#6902);
#5884=AXIS2_PLACEMENT_3D('',#8812,#6905,#6906);
#5885=AXIS2_PLACEMENT_3D('',#8815,#6909,#6910);
#5886=AXIS2_PLACEMENT_3D('',#8818,#6913,#6914);
#5887=AXIS2_PLACEMENT_3D('',#8821,#6917,#6918);
#5888=AXIS2_PLACEMENT_3D('',#8824,#6921,#6922);
#5889=AXIS2_PLACEMENT_3D('',#8826,#6924,#6925);
#5890=AXIS2_PLACEMENT_3D('',#8828,#6927,#6928);
#5891=AXIS2_PLACEMENT_3D('',#8829,#6929,#6930);
#5892=AXIS2_PLACEMENT_3D('',#8831,#6932,#6933);
#5893=AXIS2_PLACEMENT_3D('',#8833,#6935,#6936);
#5894=AXIS2_PLACEMENT_3D('',#8834,#6937,#6938);
#5895=AXIS2_PLACEMENT_3D('',#8836,#6940,#6941);
#5896=AXIS2_PLACEMENT_3D('',#8838,#6943,#6944);
#5897=AXIS2_PLACEMENT_3D('',#8839,#6945,#6946);
#5898=AXIS2_PLACEMENT_3D('',#8841,#6948,#6949);
#5899=AXIS2_PLACEMENT_3D('',#8843,#6951,#6952);
#5900=AXIS2_PLACEMENT_3D('',#8844,#6953,#6954);
#5901=AXIS2_PLACEMENT_3D('',#8846,#6956,#6957);
#5902=AXIS2_PLACEMENT_3D('',#8848,#6959,#6960);
#5903=AXIS2_PLACEMENT_3D('',#8849,#6961,#6962);
#5904=AXIS2_PLACEMENT_3D('',#8851,#6964,#6965);
#5905=AXIS2_PLACEMENT_3D('',#8853,#6967,#6968);
#5906=AXIS2_PLACEMENT_3D('',#8854,#6969,#6970);
#5907=AXIS2_PLACEMENT_3D('',#8856,#6972,#6973);
#5908=AXIS2_PLACEMENT_3D('',#8858,#6975,#6976);
#5909=AXIS2_PLACEMENT_3D('',#8859,#6977,#6978);
#5910=AXIS2_PLACEMENT_3D('',#8861,#6980,#6981);
#5911=AXIS2_PLACEMENT_3D('',#8863,#6983,#6984);
#5912=AXIS2_PLACEMENT_3D('',#8864,#6985,#6986);
#5913=AXIS2_PLACEMENT_3D('',#8866,#6988,#6989);
#5914=AXIS2_PLACEMENT_3D('',#8868,#6991,#6992);
#5915=AXIS2_PLACEMENT_3D('',#8869,#6993,#6994);
#5916=AXIS2_PLACEMENT_3D('',#8871,#6996,#6997);
#5917=AXIS2_PLACEMENT_3D('',#8873,#6999,#7000);
#5918=AXIS2_PLACEMENT_3D('',#8874,#7001,#7002);
#5919=AXIS2_PLACEMENT_3D('',#8876,#7004,#7005);
#5920=AXIS2_PLACEMENT_3D('',#8878,#7007,#7008);
#6505=DIRECTION('',(0.,0.,1.));
#6506=DIRECTION('',(1.,0.,0.));
#6617=DIRECTION('',(0.,-1.,0.));
#6618=DIRECTION('',(0.,0.,-1.));
#6619=DIRECTION('',(0.,1.,0.));
#6620=DIRECTION('',(0.,0.,1.));
#6621=DIRECTION('',(-1.21904419394898E-29,-1.,3.49148133884314E-15));
#6622=DIRECTION('',(0.,1.,0.));
#6623=DIRECTION('',(0.,0.,1.));
#6624=DIRECTION('',(0.,-1.,0.));
#6625=DIRECTION('',(0.,-1.,0.));
#6626=DIRECTION('',(0.,0.,-1.));
#6627=DIRECTION('',(0.,1.,0.));
#6628=DIRECTION('',(0.,0.,1.));
#6629=DIRECTION('',(-1.21904419394898E-29,-1.,3.49148133884314E-15));
#6630=DIRECTION('',(0.,1.,0.));
#6631=DIRECTION('',(0.,0.,1.));
#6632=DIRECTION('',(0.,-1.,0.));
#6633=DIRECTION('',(0.,-1.,0.));
#6634=DIRECTION('',(0.,0.,-1.));
#6635=DIRECTION('',(0.,1.,0.));
#6636=DIRECTION('',(0.,0.,1.));
#6637=DIRECTION('',(0.,1.,0.));
#6638=DIRECTION('',(0.,0.,1.));
#6639=DIRECTION('',(0.,1.,0.));
#6640=DIRECTION('',(0.,0.,1.));
#6641=DIRECTION('',(1.,0.,0.));
#6642=DIRECTION('',(0.,1.,0.));
#6643=DIRECTION('',(0.,0.,1.));
#6644=DIRECTION('',(-1.,0.,0.));
#6645=DIRECTION('',(0.,1.,0.));
#6646=DIRECTION('',(0.,0.,1.));
#6647=DIRECTION('',(-1.21904419394898E-29,-1.,3.49148133884314E-15));
#6648=DIRECTION('',(0.991444861373811,-4.55729764366563E-16,-0.130526192220048));
#6649=DIRECTION('',(-1.21904419394898E-29,-1.,3.49148133884314E-15));
#6650=DIRECTION('',(0.991444861373811,-4.55729764366563E-16,-0.130526192220048));
#6651=DIRECTION('',(-1.21904419394898E-29,-1.,3.49148133884314E-15));
#6652=DIRECTION('',(0.991444861373811,-4.55729764366563E-16,-0.130526192220048));
#6653=DIRECTION('',(0.,1.,0.));
#6654=DIRECTION('',(0.,0.,1.));
#6655=DIRECTION('',(-1.21904419394898E-29,-1.,3.49148133884314E-15));
#6656=DIRECTION('',(0.965925826289069,-9.03661866112653E-16,-0.258819045102518));
#6657=DIRECTION('',(-1.21904419394898E-29,-1.,3.49148133884314E-15));
#6658=DIRECTION('',(0.965925826289069,-9.03661866112653E-16,-0.258819045102518));
#6659=DIRECTION('',(-1.21904419394898E-29,-1.,3.49148133884314E-15));
#6660=DIRECTION('',(0.965925826289069,-9.03661866112653E-16,-0.258819045102518));
#6661=DIRECTION('',(0.,1.,0.));
#6662=DIRECTION('',(0.,0.,1.));
#6663=DIRECTION('',(-1.21904419394898E-29,-1.,3.49148133884314E-15));
#6664=DIRECTION('',(0.923879532511288,-1.33613206278715E-15,-0.382683432365088));
#6665=DIRECTION('',(-1.21904419394898E-29,-1.,3.49148133884314E-15));
#6666=DIRECTION('',(0.923879532511288,-1.33613206278715E-15,-0.382683432365088));
#6667=DIRECTION('',(-1.21904419394898E-29,-1.,3.49148133884314E-15));
#6668=DIRECTION('',(0.923879532511288,-1.33613206278715E-15,-0.382683432365088));
#6669=DIRECTION('',(0.,1.,0.));
#6670=DIRECTION('',(0.,0.,1.));
#6671=DIRECTION('',(-1.21904419394898E-29,-1.,3.49148133884314E-15));
#6672=DIRECTION('',(0.86602540378444,-1.74574066942157E-15,-0.5));
#6673=DIRECTION('',(-1.21904419394898E-29,-1.,3.49148133884314E-15));
#6674=DIRECTION('',(0.86602540378444,-1.74574066942157E-15,-0.5));
#6675=DIRECTION('',(-1.21904419394898E-29,-1.,3.49148133884314E-15));
#6676=DIRECTION('',(0.86602540378444,-1.74574066942157E-15,-0.5));
#6677=DIRECTION('',(0.,1.,0.));
#6678=DIRECTION('',(0.,0.,1.));
#6679=DIRECTION('',(-1.21904419394898E-29,-1.,3.49148133884314E-15));
#6680=DIRECTION('',(0.793353340291236,-2.12547916919143E-15,-0.608761429008719));
#6681=DIRECTION('',(-1.21904419394898E-29,-1.,3.49148133884314E-15));
#6682=DIRECTION('',(0.793353340291236,-2.12547916919143E-15,-0.608761429008719));
#6683=DIRECTION('',(-1.21904419394898E-29,-1.,3.49148133884314E-15));
#6684=DIRECTION('',(0.793353340291236,-2.12547916919143E-15,-0.608761429008719));
#6685=DIRECTION('',(0.,1.,0.));
#6686=DIRECTION('',(0.,0.,1.));
#6687=DIRECTION('',(-1.21904419394898E-29,-1.,3.49148133884314E-15));
#6688=DIRECTION('',(0.707106781186549,-2.46885013108227E-15,-0.707106781186547));
#6689=DIRECTION('',(-1.21904419394898E-29,-1.,3.49148133884314E-15));
#6690=DIRECTION('',(0.707106781186549,-2.46885013108227E-15,-0.707106781186547));
#6691=DIRECTION('',(-1.21904419394898E-29,-1.,3.49148133884314E-15));
#6692=DIRECTION('',(0.707106781186549,-2.46885013108227E-15,-0.707106781186547));
#6693=DIRECTION('',(0.,1.,0.));
#6694=DIRECTION('',(0.,0.,1.));
#6695=DIRECTION('',(-1.21904419394898E-29,-1.,3.49148133884314E-15));
#6696=DIRECTION('',(0.608761429008722,-2.76997838273572E-15,-0.793353340291234));
#6697=DIRECTION('',(-1.21904419394898E-29,-1.,3.49148133884314E-15));
#6698=DIRECTION('',(0.608761429008722,-2.76997838273572E-15,-0.793353340291234));
#6699=DIRECTION('',(-1.21904419394898E-29,-1.,3.49148133884314E-15));
#6700=DIRECTION('',(0.608761429008722,-2.76997838273572E-15,-0.793353340291234));
#6701=DIRECTION('',(0.,1.,0.));
#6702=DIRECTION('',(0.,0.,1.));
#6703=DIRECTION('',(-1.21904419394898E-29,-1.,3.49148133884314E-15));
#6704=DIRECTION('',(0.5,-3.02371153627746E-15,-0.866025403784438));
#6705=DIRECTION('',(-1.21904419394898E-29,-1.,3.49148133884314E-15));
#6706=DIRECTION('',(0.5,-3.02371153627746E-15,-0.866025403784438));
#6707=DIRECTION('',(-1.21904419394898E-29,-1.,3.49148133884314E-15));
#6708=DIRECTION('',(0.5,-3.02371153627746E-15,-0.866025403784438));
#6709=DIRECTION('',(0.,1.,0.));
#6710=DIRECTION('',(0.,0.,1.));
#6711=DIRECTION('',(-1.21904419394898E-29,-1.,3.49148133884314E-15));
#6712=DIRECTION('',(0.382683432365091,-3.22570814710228E-15,-0.923879532511286));
#6713=DIRECTION('',(-1.21904419394898E-29,-1.,3.49148133884314E-15));
#6714=DIRECTION('',(0.382683432365091,-3.22570814710228E-15,-0.923879532511286));
#6715=DIRECTION('',(-1.21904419394898E-29,-1.,3.49148133884314E-15));
#6716=DIRECTION('',(0.382683432365091,-3.22570814710228E-15,-0.923879532511286));
#6717=DIRECTION('',(0.,1.,0.));
#6718=DIRECTION('',(0.,0.,1.));
#6719=DIRECTION('',(-1.21904419394898E-29,-1.,3.49148133884314E-15));
#6720=DIRECTION('',(0.258819045102522,-3.37251199719492E-15,-0.965925826289068));
#6721=DIRECTION('',(-1.21904419394898E-29,-1.,3.49148133884314E-15));
#6722=DIRECTION('',(0.258819045102522,-3.37251199719492E-15,-0.965925826289068));
#6723=DIRECTION('',(-1.21904419394898E-29,-1.,3.49148133884314E-15));
#6724=DIRECTION('',(0.258819045102522,-3.37251199719492E-15,-0.965925826289068));
#6725=DIRECTION('',(0.,1.,0.));
#6726=DIRECTION('',(0.,0.,1.));
#6727=DIRECTION('',(-1.21904419394898E-29,-1.,3.49148133884314E-15));
#6728=DIRECTION('',(0.130526192220052,-3.46161123197858E-15,-0.99144486137381));
#6729=DIRECTION('',(-1.21904419394898E-29,-1.,3.49148133884314E-15));
#6730=DIRECTION('',(0.130526192220052,-3.46161123197858E-15,-0.99144486137381));
#6731=DIRECTION('',(-1.21904419394898E-29,-1.,3.49148133884314E-15));
#6732=DIRECTION('',(0.130526192220052,-3.46161123197858E-15,-0.99144486137381));
#6733=DIRECTION('',(0.866025403784439,0.,0.5));
#6734=DIRECTION('',(0.,1.,0.));
#6735=DIRECTION('',(0.,0.,1.));
#6736=DIRECTION('',(1.,0.,-1.91967175081904E-16));
#6737=DIRECTION('',(0.,1.,0.));
#6738=DIRECTION('',(0.,0.,1.));
#6739=DIRECTION('',(-1.,0.,0.));
#6740=DIRECTION('',(0.,-1.,0.));
#6741=DIRECTION('',(0.,0.,1.));
#6742=DIRECTION('',(0.,-1.,0.));
#6743=DIRECTION('',(0.,0.,1.));
#6744=DIRECTION('',(0.,1.,0.));
#6745=DIRECTION('',(0.,0.,1.));
#6746=DIRECTION('',(0.,1.,0.));
#6747=DIRECTION('',(0.,0.,1.));
#6748=DIRECTION('',(0.,-1.,0.));
#6749=DIRECTION('',(0.,0.,1.));
#6750=DIRECTION('',(0.,-1.,0.));
#6751=DIRECTION('',(0.,0.,1.));
#6752=DIRECTION('',(-1.,0.,0.));
#6753=DIRECTION('',(0.,1.,0.));
#6754=DIRECTION('',(0.,0.,1.));
#6755=DIRECTION('',(1.,0.,-1.91967175081904E-16));
#6756=DIRECTION('',(0.,1.,0.));
#6757=DIRECTION('',(0.,0.,1.));
#6758=DIRECTION('',(0.866025403784439,0.,0.5));
#6759=DIRECTION('',(0.,1.,0.));
#6760=DIRECTION('',(0.,0.,1.));
#6761=DIRECTION('',(0.,1.,0.));
#6762=DIRECTION('',(0.,0.,1.));
#6763=DIRECTION('',(0.,1.,0.));
#6764=DIRECTION('',(0.,0.,1.));
#6765=DIRECTION('',(0.,1.,0.));
#6766=DIRECTION('',(0.,0.,1.));
#6767=DIRECTION('',(0.,1.,0.));
#6768=DIRECTION('',(0.,0.,1.));
#6769=DIRECTION('',(0.,1.,0.));
#6770=DIRECTION('',(0.,0.,1.));
#6771=DIRECTION('',(0.,1.,0.));
#6772=DIRECTION('',(0.,0.,1.));
#6773=DIRECTION('',(0.,1.,0.));
#6774=DIRECTION('',(0.,0.,1.));
#6775=DIRECTION('',(0.,1.,0.));
#6776=DIRECTION('',(0.,0.,1.));
#6777=DIRECTION('',(0.,1.,0.));
#6778=DIRECTION('',(0.,0.,1.));
#6779=DIRECTION('',(0.,1.,0.));
#6780=DIRECTION('',(0.,0.,1.));
#6781=DIRECTION('',(0.,1.,0.));
#6782=DIRECTION('',(0.,0.,1.));
#6783=DIRECTION('',(0.,1.,0.));
#6784=DIRECTION('',(0.,0.,1.));
#6785=DIRECTION('',(0.,1.,0.));
#6786=DIRECTION('',(0.,0.,1.));
#6787=DIRECTION('',(0.,1.,0.));
#6788=DIRECTION('',(0.,0.,1.));
#6789=DIRECTION('',(0.,1.,0.));
#6790=DIRECTION('',(0.,0.,1.));
#6791=DIRECTION('',(0.,1.,0.));
#6792=DIRECTION('',(0.,0.,1.));
#6793=DIRECTION('',(0.,1.,0.));
#6794=DIRECTION('',(0.,0.,1.));
#6795=DIRECTION('',(0.,1.,0.));
#6796=DIRECTION('',(0.,0.,1.));
#6797=DIRECTION('',(0.,1.,0.));
#6798=DIRECTION('',(0.,0.,1.));
#6799=DIRECTION('',(0.,1.,0.));
#6800=DIRECTION('',(0.,0.,1.));
#6801=DIRECTION('',(0.,1.,0.));
#6802=DIRECTION('',(0.,0.,1.));
#6803=DIRECTION('',(0.,1.,0.));
#6804=DIRECTION('',(0.,0.,1.));
#6805=DIRECTION('',(0.,1.,0.));
#6806=DIRECTION('',(0.,0.,1.));
#6807=DIRECTION('',(0.,1.,0.));
#6808=DIRECTION('',(0.,0.,1.));
#6809=DIRECTION('',(0.,1.,0.));
#6810=DIRECTION('',(0.,0.,1.));
#6811=DIRECTION('',(0.,1.,0.));
#6812=DIRECTION('',(0.,0.,1.));
#6813=DIRECTION('',(0.,1.,0.));
#6814=DIRECTION('',(0.,0.,1.));
#6815=DIRECTION('',(0.,1.,0.));
#6816=DIRECTION('',(0.,0.,1.));
#6817=DIRECTION('',(0.,1.,0.));
#6818=DIRECTION('',(0.,0.,1.));
#6819=DIRECTION('',(0.,1.,0.));
#6820=DIRECTION('',(0.,0.,1.));
#6821=DIRECTION('',(0.,1.,0.));
#6822=DIRECTION('',(0.,0.,1.));
#6823=DIRECTION('',(0.,1.,0.));
#6824=DIRECTION('',(0.,0.,1.));
#6825=DIRECTION('',(0.,1.,0.));
#6826=DIRECTION('',(0.,0.,1.));
#6827=DIRECTION('',(0.,1.,0.));
#6828=DIRECTION('',(0.,0.,1.));
#6829=DIRECTION('',(0.,1.,0.));
#6830=DIRECTION('',(0.,0.,1.));
#6831=DIRECTION('',(0.,1.,0.));
#6832=DIRECTION('',(0.,0.,1.));
#6833=DIRECTION('',(0.,1.,0.));
#6834=DIRECTION('',(0.,0.,1.));
#6835=DIRECTION('',(0.,1.,0.));
#6836=DIRECTION('',(0.,0.,1.));
#6837=DIRECTION('',(0.,1.,0.));
#6838=DIRECTION('',(0.,0.,1.));
#6839=DIRECTION('',(0.,1.,0.));
#6840=DIRECTION('',(0.,0.,1.));
#6841=DIRECTION('',(0.,1.,0.));
#6842=DIRECTION('',(0.,0.,1.));
#6843=DIRECTION('',(0.,1.,0.));
#6844=DIRECTION('',(0.,0.,1.));
#6845=DIRECTION('',(1.,0.,0.));
#6846=DIRECTION('',(0.,1.,0.));
#6847=DIRECTION('',(0.,0.,1.));
#6848=DIRECTION('',(-1.,0.,0.));
#6849=DIRECTION('',(0.5,0.,-0.866025403784439));
#6850=DIRECTION('',(-0.866025403784439,0.,-0.5));
#6851=DIRECTION('',(0.,-1.,0.));
#6852=DIRECTION('',(0.,-1.,0.));
#6853=DIRECTION('',(0.,0.,-1.));
#6854=DIRECTION('',(0.,-1.,0.));
#6855=DIRECTION('',(0.,-1.,0.));
#6856=DIRECTION('',(0.,0.,-1.));
#6857=DIRECTION('',(0.,-1.,0.));
#6858=DIRECTION('',(0.,0.,1.));
#6859=DIRECTION('',(1.,0.,0.));
#6860=DIRECTION('',(0.,-1.,0.));
#6861=DIRECTION('',(0.,-1.,0.));
#6862=DIRECTION('',(0.,0.,-1.));
#6863=DIRECTION('',(0.,-1.,0.));
#6864=DIRECTION('',(-1.91967175081904E-16,0.,-1.));
#6865=DIRECTION('',(-1.,0.,1.91967175081904E-16));
#6866=DIRECTION('',(0.,-1.,0.));
#6867=DIRECTION('',(0.,-1.,0.));
#6868=DIRECTION('',(0.,0.,-1.));
#6869=DIRECTION('',(0.,-1.,0.));
#6870=DIRECTION('',(0.,0.,-1.));
#6871=DIRECTION('',(0.,-1.,0.));
#6872=DIRECTION('',(0.,-1.,0.));
#6873=DIRECTION('',(0.,0.,-1.));
#6874=DIRECTION('',(-1.,0.,0.));
#6875=DIRECTION('',(0.,-1.,0.));
#6876=DIRECTION('',(0.,-1.,0.));
#6877=DIRECTION('',(0.,0.,-1.));
#6878=DIRECTION('',(0.,-1.,0.));
#6879=DIRECTION('',(0.,0.,1.));
#6880=DIRECTION('',(1.,0.,0.));
#6881=DIRECTION('',(0.,-1.,0.));
#6882=DIRECTION('',(0.,0.,-1.));
#6883=DIRECTION('',(-1.21904419394898E-29,-1.,3.49148133884314E-15));
#6884=DIRECTION('',(-1.21904419394898E-29,-1.,3.49148133884314E-15));
#6885=DIRECTION('',(0.,-1.,0.));
#6886=DIRECTION('',(0.,0.,-1.));
#6887=DIRECTION('',(-1.21904419394898E-29,-1.,3.49148133884314E-15));
#6888=DIRECTION('',(-1.21904419394898E-29,-1.,3.49148133884314E-15));
#6889=DIRECTION('',(0.,-1.,0.));
#6890=DIRECTION('',(0.,0.,-1.));
#6891=DIRECTION('',(-1.21904419394898E-29,-1.,3.49148133884314E-15));
#6892=DIRECTION('',(-1.21904419394898E-29,-1.,3.49148133884314E-15));
#6893=DIRECTION('',(0.,-1.,0.));
#6894=DIRECTION('',(0.,0.,-1.));
#6895=DIRECTION('',(-1.21904419394898E-29,-1.,3.49148133884314E-15));
#6896=DIRECTION('',(-1.21904419394898E-29,-1.,3.49148133884314E-15));
#6897=DIRECTION('',(0.,-1.,0.));
#6898=DIRECTION('',(0.,0.,-1.));
#6899=DIRECTION('',(-1.21904419394898E-29,-1.,3.49148133884314E-15));
#6900=DIRECTION('',(-1.21904419394898E-29,-1.,3.49148133884314E-15));
#6901=DIRECTION('',(0.,-1.,0.));
#6902=DIRECTION('',(0.,0.,-1.));
#6903=DIRECTION('',(-1.21904419394898E-29,-1.,3.49148133884314E-15));
#6904=DIRECTION('',(-1.21904419394898E-29,-1.,3.49148133884314E-15));
#6905=DIRECTION('',(0.,-1.,0.));
#6906=DIRECTION('',(0.,0.,-1.));
#6907=DIRECTION('',(-1.21904419394898E-29,-1.,3.49148133884314E-15));
#6908=DIRECTION('',(-1.21904419394898E-29,-1.,3.49148133884314E-15));
#6909=DIRECTION('',(0.,-1.,0.));
#6910=DIRECTION('',(0.,0.,-1.));
#6911=DIRECTION('',(-1.21904419394898E-29,-1.,3.49148133884314E-15));
#6912=DIRECTION('',(-1.21904419394898E-29,-1.,3.49148133884314E-15));
#6913=DIRECTION('',(0.,-1.,0.));
#6914=DIRECTION('',(0.,0.,-1.));
#6915=DIRECTION('',(-1.21904419394898E-29,-1.,3.49148133884314E-15));
#6916=DIRECTION('',(-1.21904419394898E-29,-1.,3.49148133884314E-15));
#6917=DIRECTION('',(0.,-1.,0.));
#6918=DIRECTION('',(0.,0.,-1.));
#6919=DIRECTION('',(-1.21904419394898E-29,-1.,3.49148133884314E-15));
#6920=DIRECTION('',(-1.21904419394898E-29,-1.,3.49148133884314E-15));
#6921=DIRECTION('',(-1.21904419394898E-29,-1.,3.49148133884314E-15));
#6922=DIRECTION('',(-1.,0.,-3.49148133884314E-15));
#6923=DIRECTION('',(-1.21904419394898E-29,-1.,3.49148133884314E-15));
#6924=DIRECTION('',(-1.21904419394898E-29,-1.,3.49148133884314E-15));
#6925=DIRECTION('',(-1.,0.,-3.49148133884314E-15));
#6926=DIRECTION('',(-1.21904419394898E-29,-1.,3.49148133884314E-15));
#6927=DIRECTION('',(-1.21904419394898E-29,-1.,3.49148133884314E-15));
#6928=DIRECTION('',(-1.,0.,-3.49148133884314E-15));
#6929=DIRECTION('',(-1.21904419394898E-29,-1.,3.49148133884314E-15));
#6930=DIRECTION('',(-1.,0.,-3.49148133884314E-15));
#6931=DIRECTION('',(-1.21904419394898E-29,-1.,3.49148133884314E-15));
#6932=DIRECTION('',(-1.21904419394898E-29,-1.,3.49148133884314E-15));
#6933=DIRECTION('',(-1.,0.,-3.49148133884314E-15));
#6934=DIRECTION('',(-1.21904419394898E-29,-1.,3.49148133884314E-15));
#6935=DIRECTION('',(-1.21904419394898E-29,-1.,3.49148133884314E-15));
#6936=DIRECTION('',(-1.,0.,-3.49148133884314E-15));
#6937=DIRECTION('',(-1.21904419394898E-29,-1.,3.49148133884314E-15));
#6938=DIRECTION('',(-1.,0.,-3.49148133884314E-15));
#6939=DIRECTION('',(-1.21904419394898E-29,-1.,3.49148133884314E-15));
#6940=DIRECTION('',(-1.21904419394898E-29,-1.,3.49148133884314E-15));
#6941=DIRECTION('',(-1.,0.,-3.49148133884314E-15));
#6942=DIRECTION('',(-1.21904419394898E-29,-1.,3.49148133884314E-15));
#6943=DIRECTION('',(-1.21904419394898E-29,-1.,3.49148133884314E-15));
#6944=DIRECTION('',(-1.,0.,-3.49148133884314E-15));
#6945=DIRECTION('',(-1.21904419394898E-29,-1.,3.49148133884314E-15));
#6946=DIRECTION('',(-1.,0.,-3.49148133884314E-15));
#6947=DIRECTION('',(-1.21904419394898E-29,-1.,3.49148133884314E-15));
#6948=DIRECTION('',(-1.21904419394898E-29,-1.,3.49148133884314E-15));
#6949=DIRECTION('',(-1.,0.,-3.49148133884314E-15));
#6950=DIRECTION('',(-1.21904419394898E-29,-1.,3.49148133884314E-15));
#6951=DIRECTION('',(-1.21904419394898E-29,-1.,3.49148133884314E-15));
#6952=DIRECTION('',(-1.,0.,-3.49148133884314E-15));
#6953=DIRECTION('',(-1.21904419394898E-29,-1.,3.49148133884314E-15));
#6954=DIRECTION('',(-1.,0.,-3.49148133884314E-15));
#6955=DIRECTION('',(-1.21904419394898E-29,-1.,3.49148133884314E-15));
#6956=DIRECTION('',(-1.21904419394898E-29,-1.,3.49148133884314E-15));
#6957=DIRECTION('',(-1.,0.,-3.49148133884314E-15));
#6958=DIRECTION('',(-1.21904419394898E-29,-1.,3.49148133884314E-15));
#6959=DIRECTION('',(-1.21904419394898E-29,-1.,3.49148133884314E-15));
#6960=DIRECTION('',(-1.,0.,-3.49148133884314E-15));
#6961=DIRECTION('',(-1.21904419394898E-29,-1.,3.49148133884314E-15));
#6962=DIRECTION('',(-1.,0.,-3.49148133884314E-15));
#6963=DIRECTION('',(-1.21904419394898E-29,-1.,3.49148133884314E-15));
#6964=DIRECTION('',(-1.21904419394898E-29,-1.,3.49148133884314E-15));
#6965=DIRECTION('',(-1.,0.,-3.49148133884314E-15));
#6966=DIRECTION('',(-1.21904419394898E-29,-1.,3.49148133884314E-15));
#6967=DIRECTION('',(-1.21904419394898E-29,-1.,3.49148133884314E-15));
#6968=DIRECTION('',(-1.,0.,-3.49148133884314E-15));
#6969=DIRECTION('',(-1.21904419394898E-29,-1.,3.49148133884314E-15));
#6970=DIRECTION('',(-1.,0.,-3.49148133884314E-15));
#6971=DIRECTION('',(-1.21904419394898E-29,-1.,3.49148133884314E-15));
#6972=DIRECTION('',(-1.21904419394898E-29,-1.,3.49148133884314E-15));
#6973=DIRECTION('',(-1.,0.,-3.49148133884314E-15));
#6974=DIRECTION('',(-1.21904419394898E-29,-1.,3.49148133884314E-15));
#6975=DIRECTION('',(-1.21904419394898E-29,-1.,3.49148133884314E-15));
#6976=DIRECTION('',(-1.,0.,-3.49148133884314E-15));
#6977=DIRECTION('',(-1.21904419394898E-29,-1.,3.49148133884314E-15));
#6978=DIRECTION('',(-1.,0.,-3.49148133884314E-15));
#6979=DIRECTION('',(-1.21904419394898E-29,-1.,3.49148133884314E-15));
#6980=DIRECTION('',(-1.21904419394898E-29,-1.,3.49148133884314E-15));
#6981=DIRECTION('',(-1.,0.,-3.49148133884314E-15));
#6982=DIRECTION('',(-1.21904419394898E-29,-1.,3.49148133884314E-15));
#6983=DIRECTION('',(-1.21904419394898E-29,-1.,3.49148133884314E-15));
#6984=DIRECTION('',(-1.,0.,-3.49148133884314E-15));
#6985=DIRECTION('',(-1.21904419394898E-29,-1.,3.49148133884314E-15));
#6986=DIRECTION('',(-1.,0.,-3.49148133884314E-15));
#6987=DIRECTION('',(-1.21904419394898E-29,-1.,3.49148133884314E-15));
#6988=DIRECTION('',(-1.21904419394898E-29,-1.,3.49148133884314E-15));
#6989=DIRECTION('',(-1.,0.,-3.49148133884314E-15));
#6990=DIRECTION('',(-1.21904419394898E-29,-1.,3.49148133884314E-15));
#6991=DIRECTION('',(-1.21904419394898E-29,-1.,3.49148133884314E-15));
#6992=DIRECTION('',(-1.,0.,-3.49148133884314E-15));
#6993=DIRECTION('',(-1.21904419394898E-29,-1.,3.49148133884314E-15));
#6994=DIRECTION('',(-1.,0.,-3.49148133884314E-15));
#6995=DIRECTION('',(-1.21904419394898E-29,-1.,3.49148133884314E-15));
#6996=DIRECTION('',(-1.21904419394898E-29,-1.,3.49148133884314E-15));
#6997=DIRECTION('',(-1.,0.,-3.49148133884314E-15));
#6998=DIRECTION('',(-1.21904419394898E-29,-1.,3.49148133884314E-15));
#6999=DIRECTION('',(-1.21904419394898E-29,-1.,3.49148133884314E-15));
#7000=DIRECTION('',(-1.,0.,-3.49148133884314E-15));
#7001=DIRECTION('',(-1.21904419394898E-29,-1.,3.49148133884314E-15));
#7002=DIRECTION('',(-1.,0.,-3.49148133884314E-15));
#7003=DIRECTION('',(-1.21904419394898E-29,-1.,3.49148133884314E-15));
#7004=DIRECTION('',(-1.21904419394898E-29,-1.,3.49148133884314E-15));
#7005=DIRECTION('',(-1.,0.,-3.49148133884314E-15));
#7006=DIRECTION('',(-1.21904419394898E-29,-1.,3.49148133884314E-15));
#7007=DIRECTION('',(-1.21904419394898E-29,-1.,3.49148133884314E-15));
#7008=DIRECTION('',(-1.,0.,-3.49148133884314E-15));
#8391=CARTESIAN_POINT('',(0.,0.,0.));
#8536=CARTESIAN_POINT('',(0.0151554445662277,0.002,0.00875));
#8537=CARTESIAN_POINT('',(0.0151554445662277,0.,0.00875));
#8538=CARTESIAN_POINT('',(0.0151554445662277,0.,-0.00375));
#8539=CARTESIAN_POINT('',(0.0141805044897511,0.,-0.00371192167553948));
#8540=CARTESIAN_POINT('',(0.0141805044897511,-0.0005,-0.00371192167553948));
#8541=CARTESIAN_POINT('',(0.0141805044897511,0.002,-0.00371192167553948));
#8542=CARTESIAN_POINT('',(0.0151554445662277,0.002,0.00875));
#8543=CARTESIAN_POINT('',(0.0151554445662277,0.002,-0.00375));
#8544=CARTESIAN_POINT('',(0.0151554445662277,0.002,-0.00375));
#8545=CARTESIAN_POINT('',(0.0151554445662277,0.002,0.00875));
#8546=CARTESIAN_POINT('',(0.0151554445662277,0.002,0.00875));
#8547=CARTESIAN_POINT('',(0.00269352289068823,0.002,0.00777505992352337));
#8548=CARTESIAN_POINT('',(0.00265544456622767,0.002,0.00875));
#8549=CARTESIAN_POINT('',(0.00269352289068823,-0.000499999999999958,0.00777505992352337));
#8550=CARTESIAN_POINT('',(0.00269352289068823,0.,0.00777505992352337));
#8551=CARTESIAN_POINT('',(0.0151554445662277,0.,0.00875));
#8552=CARTESIAN_POINT('',(0.00265544456622767,0.,0.00875));
#8553=CARTESIAN_POINT('',(0.00265544456622767,0.002,0.00875));
#8554=CARTESIAN_POINT('',(0.0151554445662277,0.002,0.00875));
#8555=CARTESIAN_POINT('',(0.0151554445662277,0.,0.00875));
#8556=CARTESIAN_POINT('',(0.0151554445662277,0.,0.01025));
#8557=CARTESIAN_POINT('',(0.0151554445662277,0.002,0.00875));
#8558=CARTESIAN_POINT('',(0.0151554445662277,0.002,0.01025));
#8559=CARTESIAN_POINT('',(0.0477117510540525,0.002,-0.0177067054013465));
#8560=CARTESIAN_POINT('',(0.0320811989597626,0.002,0.0191786316782243));
#8561=CARTESIAN_POINT('',(0.0320811989597626,0.002,0.0191786316782243));
#8562=CARTESIAN_POINT('',(0.0449321327792465,0.002,0.0191786316782244));
#8563=CARTESIAN_POINT('',(0.0320811989597626,0.002,0.0176786316782244));
#8564=CARTESIAN_POINT('',(0.0320811989597626,0.002,0.0161786316782242));
#8565=CARTESIAN_POINT('',(0.0320811989597626,0.002,0.0161786316782242));
#8566=CARTESIAN_POINT('',(0.0449321327792465,0.002,0.0161786316782242));
#8567=CARTESIAN_POINT('',(0.0449321327792465,0.002,0.0176786316782244));
#8568=CARTESIAN_POINT('',(0.0186533102025936,0.002,-0.00197008096664466));
#8569=CARTESIAN_POINT('',(0.0138888686280741,0.002,-0.00255325888374197));
#8570=CARTESIAN_POINT('',(0.0151554445662277,0.00200000000000005,0.00875));
#8571=CARTESIAN_POINT('',(0.0134533643050099,0.002,-0.00249592365190046));
#8572=CARTESIAN_POINT('',(0.00900220469196413,0.002,-0.000699488821690833));
#8573=CARTESIAN_POINT('',(0.0128717816969752,0.002,-0.00353962505122098));
#8574=CARTESIAN_POINT('',(0.0151554445662277,0.002,0.00875));
#8575=CARTESIAN_POINT('',(0.0125622380532049,0.002,-0.00347805299223131));
#8576=CARTESIAN_POINT('',(0.017224134128312,0.002,-0.00233493227030325));
#8577=CARTESIAN_POINT('',(0.0124243330190333,0.002,-0.00229123660269913));
#8578=CARTESIAN_POINT('',(0.0151554445662277,0.00200000000000005,0.00875));
#8579=CARTESIAN_POINT('',(0.0120000382453175,0.002,-0.00217754716072923));
#8580=CARTESIAN_POINT('',(0.0078214407177674,0.002,0.000184511835729573));
#8581=CARTESIAN_POINT('',(0.0112872007876491,0.002,-0.00313640778660604));
#8582=CARTESIAN_POINT('',(0.0151554445662277,0.002,0.00875));
#8583=CARTESIAN_POINT('',(0.0109883420990692,0.002,-0.00303495893196928));
#8584=CARTESIAN_POINT('',(0.0157595622020739,0.002,-0.00251011730949313));
#8585=CARTESIAN_POINT('',(0.0110065274857722,0.002,-0.00184029570217498));
#8586=CARTESIAN_POINT('',(0.0151554445662277,0.00200000000000005,0.00875));
#8587=CARTESIAN_POINT('',(0.0106007020626198,0.002,-0.00167219730794948));
#8588=CARTESIAN_POINT('',(0.00676616358278785,0.002,0.00121507037044262));
#8589=CARTESIAN_POINT('',(0.00976880660185426,0.002,-0.00252981078922743));
#8590=CARTESIAN_POINT('',(0.0151554445662277,0.002,0.00875));
#8591=CARTESIAN_POINT('',(0.00948574642348564,0.002,-0.00239022095697335));
#8592=CARTESIAN_POINT('',(0.0142846536555935,0.002,-0.00249263861962324));
#8593=CARTESIAN_POINT('',(0.00965971107405478,0.002,-0.00120815190600194));
#8594=CARTESIAN_POINT('',(0.0151554445662277,0.00200000000000005,0.00875));
#8595=CARTESIAN_POINT('',(0.0092792987869721,0.002,-0.000988520769651722));
#8596=CARTESIAN_POINT('',(0.00585442937138308,0.00200000000000003,0.00237455364019456));
#8597=CARTESIAN_POINT('',(0.00834257928508805,0.002,-0.00173021310189077));
#8598=CARTESIAN_POINT('',(0.0151554445662277,0.002,0.00875));
#8599=CARTESIAN_POINT('',(0.0080801608550617,0.002,-0.00155487071275084));
#8600=CARTESIAN_POINT('',(0.0128246445830229,0.002,-0.00228279526592331));
#8601=CARTESIAN_POINT('',(0.00840692818609363,0.002,-0.000405621369795907));
#8602=CARTESIAN_POINT('',(0.0151554445662277,0.00200000000000005,0.00875));
#8603=CARTESIAN_POINT('',(0.00805843799478281,0.002,-0.000138215440957164));
#8604=CARTESIAN_POINT('',(0.00510183810869068,0.00200000000000003,0.00364312256477043));
#8605=CARTESIAN_POINT('',(0.00703292198216526,0.002,-0.00075129606271674));
#8606=CARTESIAN_POINT('',(0.0151554445662277,0.002,0.00875));
#8607=CARTESIAN_POINT('',(0.00679563535257506,0.002,-0.000543201273583248));
#8608=CARTESIAN_POINT('',(0.0114045161443848,0.002,-0.00188417772635469));
#8609=CARTESIAN_POINT('',(0.0072696142844388,0.002,0.000553564386465146));
#8610=CARTESIAN_POINT('',(0.0151554445662277,0.00200000000000005,0.00875));
#8611=CARTESIAN_POINT('',(0.0069590089526929,0.002,0.000864169718211046));
#8612=CARTESIAN_POINT('',(0.00452126683987305,0.00200000000000004,0.00499907157815701));
#8613=CARTESIAN_POINT('',(0.00586224329264449,0.002,0.000390190786347311));
#8614=CARTESIAN_POINT('',(0.0151554445662277,0.002,0.00875));
#8615=CARTESIAN_POINT('',(0.005654148503511,0.002,0.000627477415937518));
#8616=CARTESIAN_POINT('',(0.0100485671309982,0.002,-0.00130360645753706));
#8617=CARTESIAN_POINT('',(0.00626722912527059,0.002,0.00165299342855505));
#8618=CARTESIAN_POINT('',(0.0151554445662277,0.00200000000000005,0.00875));
#8619=CARTESIAN_POINT('',(0.00599982319643184,0.002,0.00200148361986587));
#8620=CARTESIAN_POINT('',(0.00412264930030442,0.00200000000000004,0.00641920001679515));
#8621=CARTESIAN_POINT('',(0.00485057385347689,0.002,0.00167471628883397));
#8622=CARTESIAN_POINT('',(0.0151554445662277,0.002,0.00875));
#8623=CARTESIAN_POINT('',(0.00467523146433696,0.002,0.00193713471886032));
#8624=CARTESIAN_POINT('',(0.00877999820642231,0.002,-0.000551015194844674));
#8625=CARTESIAN_POINT('',(0.00541692379657602,0.002,0.00287385422074434));
#8626=CARTESIAN_POINT('',(0.0151554445662277,0.00200000000000005,0.00875));
#8627=CARTESIAN_POINT('',(0.0051972926602258,0.002,0.00325426650782702));
#8628=CARTESIAN_POINT('',(0.00391280594660448,0.00200000000000004,0.00787920908936577));
#8629=CARTESIAN_POINT('',(0.00401522360925438,0.002,0.0030803018572579));
#8630=CARTESIAN_POINT('',(0.0151554445662277,0.002,0.00875));
#8631=CARTESIAN_POINT('',(0.00387563377700029,0.002,0.0033633620356265));
#8632=CARTESIAN_POINT('',(0.00762051493667037,0.002,0.000360719016560104));
#8633=CARTESIAN_POINT('',(0.00473324725827826,0.002,0.00419525749639209));
#8634=CARTESIAN_POINT('',(0.0151554445662277,0.00200000000000005,0.00875));
#8635=CARTESIAN_POINT('',(0.00456514886405276,0.002,0.00460108291954443));
#8636=CARTESIAN_POINT('',(0.0038953272567346,0.00200000000000005,0.00935411763584619));
#8637=CARTESIAN_POINT('',(0.00337048563425844,0.002,0.00458289753284146));
#8638=CARTESIAN_POINT('',(0.0151554445662277,0.002,0.00875));
#8639=CARTESIAN_POINT('',(0.00326903677962168,0.002,0.00488175622142132));
#8640=CARTESIAN_POINT('',(0.00658995640195732,0.002,0.00141599615153965));
#8641=CARTESIAN_POINT('',(0.0042278974054985,0.002,0.00559459367908977));
#8642=CARTESIAN_POINT('',(0.0151554445662277,0.00200000000000005,0.00875));
#8643=CARTESIAN_POINT('',(0.00411420796352861,0.002,0.00601888845280556));
#8644=CARTESIAN_POINT('',(0.00407051229592446,0.00200000000000005,0.0108186895620842));
#8645=CARTESIAN_POINT('',(0.00292739157399641,0.002,0.00615679348697717));
#8646=CARTESIAN_POINT('',(0.0151554445662277,0.002,0.00875));
#8647=CARTESIAN_POINT('',(0.00286581951500674,0.002,0.00646633713074741));
#8648=CARTESIAN_POINT('',(0.00570595574453691,0.00200000000000003,0.00259676012573636));
#8649=CARTESIAN_POINT('',(0.00390952091432728,0.002,0.00704791973878213));
#8650=CARTESIAN_POINT('',(0.0151554445662277,0.00200000000000005,0.00875));
#8651=CARTESIAN_POINT('',(0.00385218568248577,0.002,0.00748342406184637));
#8652=CARTESIAN_POINT('',(0.00443536359958305,0.00200000000000006,0.0122478656363659));
#8653=CARTESIAN_POINT('',(0.00265544456622766,0.002,0.00875));
#8654=CARTESIAN_POINT('',(0.0226789374388172,0.002,0.0203105690001062));
#8655=CARTESIAN_POINT('',(0.0301789374388172,0.002,0.00732018794333958));
#8656=CARTESIAN_POINT('',(0.0301789374388172,0.002,0.0223201879433396));
#8657=CARTESIAN_POINT('',(0.0482520634848371,0.002,0.0223201879433396));
#8658=CARTESIAN_POINT('',(0.0482520634848371,0.002,0.0223201879433396));
#8659=CARTESIAN_POINT('',(0.046393043464028,0.002,0.0176786316782243));
#8660=CARTESIAN_POINT('',(0.0482520634848371,0.002,0.0130370754131091));
#8661=CARTESIAN_POINT('',(0.0482520634848371,0.002,0.0130370754131092));
#8662=CARTESIAN_POINT('',(0.0315024131220503,0.002,0.0130370754131092));
#8663=CARTESIAN_POINT('',(0.0315024131220503,0.002,0.00803707541310922));
#8664=CARTESIAN_POINT('',(0.0288383125530301,0.002,0.0122682180670677));
#8665=CARTESIAN_POINT('',(0.0477117510540525,0.002,-0.0177067054013465));
#8666=CARTESIAN_POINT('',(0.0477117510540525,0.,-0.0177067054013465));
#8667=CARTESIAN_POINT('',(0.0186533102025936,0.,-0.00197008096664465));
#8668=CARTESIAN_POINT('',(0.0138888686280741,0.,-0.00255325888374196));
#8669=CARTESIAN_POINT('',(0.0477117510540525,0.,-0.0177067054013465));
#8670=CARTESIAN_POINT('',(0.0288383125530301,0.,0.0122682180670677));
#8671=CARTESIAN_POINT('',(0.0315024131220503,0.,0.00803707541310922));
#8672=CARTESIAN_POINT('',(0.0315024131220503,0.,0.0130370754131092));
#8673=CARTESIAN_POINT('',(0.0482520634848371,0.,0.0130370754131092));
#8674=CARTESIAN_POINT('',(0.0482520634848371,0.,0.0130370754131091));
#8675=CARTESIAN_POINT('',(0.046393043464028,0.,0.0176786316782243));
#8676=CARTESIAN_POINT('',(0.0482520634848371,0.,0.0223201879433396));
#8677=CARTESIAN_POINT('',(0.0482520634848371,0.,0.0223201879433396));
#8678=CARTESIAN_POINT('',(0.0301789374388172,0.,0.0223201879433396));
#8679=CARTESIAN_POINT('',(0.0301789374388172,0.,0.00732018794333958));
#8680=CARTESIAN_POINT('',(0.0226789374388172,0.,0.0203105690001062));
#8681=CARTESIAN_POINT('',(0.00265544456622766,0.,0.00875));
#8682=CARTESIAN_POINT('',(0.00443536359958305,0.,0.0122478656363659));
#8683=CARTESIAN_POINT('',(0.00385218568248577,0.,0.00748342406184638));
#8684=CARTESIAN_POINT('',(0.0151554445662277,0.,0.00875));
#8685=CARTESIAN_POINT('',(0.00390952091432728,0.,0.00704791973878214));
#8686=CARTESIAN_POINT('',(0.00570595574453691,0.,0.00259676012573637));
#8687=CARTESIAN_POINT('',(0.00286581951500674,0.,0.00646633713074741));
#8688=CARTESIAN_POINT('',(0.0151554445662277,0.,0.00875));
#8689=CARTESIAN_POINT('',(0.00292739157399641,0.,0.00615679348697717));
#8690=CARTESIAN_POINT('',(0.00407051229592446,0.,0.0108186895620842));
#8691=CARTESIAN_POINT('',(0.00411420796352861,0.,0.00601888845280557));
#8692=CARTESIAN_POINT('',(0.0151554445662277,0.,0.00875));
#8693=CARTESIAN_POINT('',(0.0042278974054985,0.,0.00559459367908978));
#8694=CARTESIAN_POINT('',(0.00658995640195732,0.,0.00141599615153966));
#8695=CARTESIAN_POINT('',(0.00326903677962168,0.,0.00488175622142132));
#8696=CARTESIAN_POINT('',(0.0151554445662277,0.,0.00875));
#8697=CARTESIAN_POINT('',(0.00337048563425844,0.,0.00458289753284146));
#8698=CARTESIAN_POINT('',(0.0038953272567346,0.,0.00935411763584619));
#8699=CARTESIAN_POINT('',(0.00456514886405276,0.,0.00460108291954444));
#8700=CARTESIAN_POINT('',(0.0151554445662277,0.,0.00875));
#8701=CARTESIAN_POINT('',(0.00473324725827826,0.,0.0041952574963921));
#8702=CARTESIAN_POINT('',(0.00762051493667037,0.,0.000360719016560111));
#8703=CARTESIAN_POINT('',(0.00387563377700029,0.,0.0033633620356265));
#8704=CARTESIAN_POINT('',(0.0151554445662277,0.,0.00875));
#8705=CARTESIAN_POINT('',(0.00401522360925438,0.,0.0030803018572579));
#8706=CARTESIAN_POINT('',(0.00391280594660448,0.,0.00787920908936577));
#8707=CARTESIAN_POINT('',(0.0051972926602258,0.,0.00325426650782703));
#8708=CARTESIAN_POINT('',(0.0151554445662277,0.,0.00875));
#8709=CARTESIAN_POINT('',(0.00541692379657602,0.,0.00287385422074435));
#8710=CARTESIAN_POINT('',(0.00877999820642231,0.,-0.000551015194844667));
#8711=CARTESIAN_POINT('',(0.00467523146433696,0.,0.00193713471886032));
#8712=CARTESIAN_POINT('',(0.0151554445662277,0.,0.00875));
#8713=CARTESIAN_POINT('',(0.00485057385347689,0.,0.00167471628883397));
#8714=CARTESIAN_POINT('',(0.00412264930030442,0.,0.00641920001679516));
#8715=CARTESIAN_POINT('',(0.00599982319643184,0.,0.00200148361986588));
#8716=CARTESIAN_POINT('',(0.0151554445662277,0.,0.00875));
#8717=CARTESIAN_POINT('',(0.00626722912527059,0.,0.00165299342855506));
#8718=CARTESIAN_POINT('',(0.0100485671309982,0.,-0.00130360645753706));
#8719=CARTESIAN_POINT('',(0.005654148503511,0.,0.000627477415937518));
#8720=CARTESIAN_POINT('',(0.0151554445662277,0.,0.00875));
#8721=CARTESIAN_POINT('',(0.00586224329264449,0.,0.000390190786347311));
#8722=CARTESIAN_POINT('',(0.00452126683987305,0.,0.00499907157815702));
#8723=CARTESIAN_POINT('',(0.0069590089526929,0.,0.000864169718211053));
#8724=CARTESIAN_POINT('',(0.0151554445662277,0.,0.00875));
#8725=CARTESIAN_POINT('',(0.0072696142844388,0.,0.000553564386465153));
#8726=CARTESIAN_POINT('',(0.0114045161443848,0.,-0.00188417772635469));
#8727=CARTESIAN_POINT('',(0.00679563535257506,0.,-0.000543201273583248));
#8728=CARTESIAN_POINT('',(0.0151554445662277,0.,0.00875));
#8729=CARTESIAN_POINT('',(0.00703292198216526,0.,-0.00075129606271674));
#8730=CARTESIAN_POINT('',(0.00510183810869068,0.,0.00364312256477044));
#8731=CARTESIAN_POINT('',(0.00805843799478281,0.,-0.000138215440957157));
#8732=CARTESIAN_POINT('',(0.0151554445662277,0.,0.00875));
#8733=CARTESIAN_POINT('',(0.00840692818609363,0.,-0.0004056213697959));
#8734=CARTESIAN_POINT('',(0.0128246445830229,0.,-0.0022827952659233));
#8735=CARTESIAN_POINT('',(0.0080801608550617,0.,-0.00155487071275084));
#8736=CARTESIAN_POINT('',(0.0151554445662277,0.,0.00875));
#8737=CARTESIAN_POINT('',(0.00834257928508805,0.,-0.00173021310189077));
#8738=CARTESIAN_POINT('',(0.00585442937138308,0.,0.00237455364019457));
#8739=CARTESIAN_POINT('',(0.0092792987869721,0.,-0.000988520769651714));
#8740=CARTESIAN_POINT('',(0.0151554445662277,0.,0.00875));
#8741=CARTESIAN_POINT('',(0.00965971107405478,0.,-0.00120815190600194));
#8742=CARTESIAN_POINT('',(0.0142846536555935,0.,-0.00249263861962324));
#8743=CARTESIAN_POINT('',(0.00948574642348564,0.,-0.00239022095697335));
#8744=CARTESIAN_POINT('',(0.0151554445662277,0.,0.00875));
#8745=CARTESIAN_POINT('',(0.00976880660185426,0.,-0.00252981078922743));
#8746=CARTESIAN_POINT('',(0.00676616358278785,0.,0.00121507037044262));
#8747=CARTESIAN_POINT('',(0.0106007020626198,0.,-0.00167219730794947));
#8748=CARTESIAN_POINT('',(0.0151554445662277,0.,0.00875));
#8749=CARTESIAN_POINT('',(0.0110065274857722,0.,-0.00184029570217498));
#8750=CARTESIAN_POINT('',(0.0157595622020739,0.,-0.00251011730949312));
#8751=CARTESIAN_POINT('',(0.0109883420990692,0.,-0.00303495893196928));
#8752=CARTESIAN_POINT('',(0.0151554445662277,0.,0.00875));
#8753=CARTESIAN_POINT('',(0.0112872007876491,0.,-0.00313640778660604));
#8754=CARTESIAN_POINT('',(0.0078214407177674,0.,0.00018451183572958));
#8755=CARTESIAN_POINT('',(0.0120000382453175,0.,-0.00217754716072922));
#8756=CARTESIAN_POINT('',(0.0151554445662277,0.,0.00875));
#8757=CARTESIAN_POINT('',(0.0124243330190333,0.,-0.00229123660269911));
#8758=CARTESIAN_POINT('',(0.017224134128312,0.,-0.00233493227030325));
#8759=CARTESIAN_POINT('',(0.0125622380532049,0.,-0.00347805299223131));
#8760=CARTESIAN_POINT('',(0.0151554445662277,0.,0.00875));
#8761=CARTESIAN_POINT('',(0.0128717816969752,0.,-0.00353962505122098));
#8762=CARTESIAN_POINT('',(0.00900220469196413,0.,-0.000699488821690826));
#8763=CARTESIAN_POINT('',(0.0134533643050099,0.,-0.00249592365190045));
#8764=CARTESIAN_POINT('',(0.0151554445662277,0.,0.00875));
#8765=CARTESIAN_POINT('',(0.0320811989597626,0.,0.0176786316782244));
#8766=CARTESIAN_POINT('',(0.0320811989597626,0.,0.0161786316782242));
#8767=CARTESIAN_POINT('',(0.0320811989597626,0.,0.0191786316782243));
#8768=CARTESIAN_POINT('',(0.0320811989597626,0.,0.0191786316782243));
#8769=CARTESIAN_POINT('',(0.0449321327792465,0.,0.0191786316782244));
#8770=CARTESIAN_POINT('',(0.0449321327792465,0.,0.0176786316782244));
#8771=CARTESIAN_POINT('',(0.0449321327792465,0.,0.0161786316782242));
#8772=CARTESIAN_POINT('',(0.0320811989597626,0.,0.0161786316782242));
#8773=CARTESIAN_POINT('',(0.00265544456622766,0.002,0.00875));
#8774=CARTESIAN_POINT('',(0.0226789374388172,0.002,0.0203105690001062));
#8775=CARTESIAN_POINT('',(0.0477117510540525,0.002,-0.0177067054013465));
#8776=CARTESIAN_POINT('',(0.0288383125530301,0.002,0.0122682180670677));
#8777=CARTESIAN_POINT('',(0.0315024131220503,0.002,0.00803707541310922));
#8778=CARTESIAN_POINT('',(0.0315024131220503,0.002,0.0130370754131092));
#8779=CARTESIAN_POINT('',(0.0482520634848371,0.002,0.0130370754131092));
#8780=CARTESIAN_POINT('',(0.0482520634848371,0.002,0.0130370754131091));
#8781=CARTESIAN_POINT('',(0.046393043464028,0.002,0.0176786316782243));
#8782=CARTESIAN_POINT('',(0.0482520634848371,0.002,0.0223201879433396));
#8783=CARTESIAN_POINT('',(0.0482520634848371,0.002,0.0223201879433396));
#8784=CARTESIAN_POINT('',(0.0301789374388172,0.002,0.0223201879433396));
#8785=CARTESIAN_POINT('',(0.0301789374388172,0.002,0.00732018794333958));
#8786=CARTESIAN_POINT('',(0.0320811989597626,0.002,0.0176786316782244));
#8787=CARTESIAN_POINT('',(0.0320811989597626,0.002,0.0161786316782242));
#8788=CARTESIAN_POINT('',(0.0320811989597626,0.002,0.0191786316782243));
#8789=CARTESIAN_POINT('',(0.0320811989597626,0.002,0.0191786316782243));
#8790=CARTESIAN_POINT('',(0.0449321327792465,0.002,0.0191786316782244));
#8791=CARTESIAN_POINT('',(0.0449321327792465,0.002,0.0176786316782244));
#8792=CARTESIAN_POINT('',(0.0449321327792465,0.002,0.0161786316782242));
#8793=CARTESIAN_POINT('',(0.0320811989597626,0.002,0.0161786316782242));
#8794=CARTESIAN_POINT('',(0.0151554445662277,0.002,0.00875));
#8795=CARTESIAN_POINT('',(0.00292739157399641,-0.000499999999999964,0.00615679348697716));
#8796=CARTESIAN_POINT('',(0.00286581951500674,-0.000499999999999964,0.00646633713074741));
#8797=CARTESIAN_POINT('',(0.0151554445662277,0.002,0.00875));
#8798=CARTESIAN_POINT('',(0.00337048563425845,-0.000499999999999969,0.00458289753284145));
#8799=CARTESIAN_POINT('',(0.00326903677962168,-0.000499999999999969,0.00488175622142132));
#8800=CARTESIAN_POINT('',(0.0151554445662277,0.002,0.00875));
#8801=CARTESIAN_POINT('',(0.00387563377700029,-0.000499999999999973,0.0033633620356265));
#8802=CARTESIAN_POINT('',(0.00401522360925438,-0.000499999999999975,0.0030803018572579));
#8803=CARTESIAN_POINT('',(0.0151554445662277,0.002,0.00875));
#8804=CARTESIAN_POINT('',(0.00467523146433696,-0.000499999999999979,0.00193713471886031));
#8805=CARTESIAN_POINT('',(0.00485057385347689,-0.00049999999999998,0.00167471628883396));
#8806=CARTESIAN_POINT('',(0.0151554445662277,0.002,0.00875));
#8807=CARTESIAN_POINT('',(0.00586224329264449,-0.000499999999999983,0.000390190786347312));
#8808=CARTESIAN_POINT('',(0.005654148503511,-0.000499999999999982,0.000627477415937519));
#8809=CARTESIAN_POINT('',(0.0151554445662277,0.002,0.00875));
#8810=CARTESIAN_POINT('',(0.00703292198216527,-0.000499999999999989,-0.000751296062716742));
#8811=CARTESIAN_POINT('',(0.00679563535257506,-0.000499999999999986,-0.000543201273583248));
#8812=CARTESIAN_POINT('',(0.0151554445662277,0.002,0.00875));
#8813=CARTESIAN_POINT('',(0.00808016085506171,-0.00049999999999999,-0.00155487071275084));
#8814=CARTESIAN_POINT('',(0.00834257928508806,-0.000499999999999991,-0.00173021310189077));
#8815=CARTESIAN_POINT('',(0.0151554445662277,0.002,0.00875));
#8816=CARTESIAN_POINT('',(0.00976880660185426,-0.000499999999999994,-0.00252981078922743));
#8817=CARTESIAN_POINT('',(0.00948574642348565,-0.000499999999999994,-0.00239022095697335));
#8818=CARTESIAN_POINT('',(0.0151554445662277,0.002,0.00875));
#8819=CARTESIAN_POINT('',(0.0112872007876491,-0.0005,-0.00313640778660604));
#8820=CARTESIAN_POINT('',(0.0109883420990692,-0.0005,-0.00303495893196928));
#8821=CARTESIAN_POINT('',(0.0151554445662277,0.002,0.00875));
#8822=CARTESIAN_POINT('',(0.0128717816969752,-0.0005,-0.00353962505122098));
#8823=CARTESIAN_POINT('',(0.0125622380532049,-0.0005,-0.00347805299223131));
#8824=CARTESIAN_POINT('',(0.0186533102025936,0.002,-0.00197008096664466));
#8825=CARTESIAN_POINT('',(0.0138888686280741,0.002,-0.00255325888374197));
#8826=CARTESIAN_POINT('',(0.0151554445662277,0.00200000000000005,0.00875));
#8827=CARTESIAN_POINT('',(0.0134533643050099,0.002,-0.00249592365190045));
#8828=CARTESIAN_POINT('',(0.00900220469196413,0.002,-0.000699488821690833));
#8829=CARTESIAN_POINT('',(0.017224134128312,0.002,-0.00233493227030325));
#8830=CARTESIAN_POINT('',(0.0124243330190333,0.002,-0.00229123660269913));
#8831=CARTESIAN_POINT('',(0.0151554445662277,0.00200000000000005,0.00875));
#8832=CARTESIAN_POINT('',(0.0120000382453175,0.002,-0.00217754716072923));
#8833=CARTESIAN_POINT('',(0.0078214407177674,0.002,0.000184511835729573));
#8834=CARTESIAN_POINT('',(0.0157595622020739,0.002,-0.00251011730949313));
#8835=CARTESIAN_POINT('',(0.0110065274857722,0.002,-0.00184029570217498));
#8836=CARTESIAN_POINT('',(0.0151554445662277,0.00200000000000005,0.00875));
#8837=CARTESIAN_POINT('',(0.0106007020626198,0.002,-0.00167219730794948));
#8838=CARTESIAN_POINT('',(0.00676616358278785,0.002,0.00121507037044262));
#8839=CARTESIAN_POINT('',(0.0142846536555935,0.002,-0.00249263861962324));
#8840=CARTESIAN_POINT('',(0.00965971107405478,0.002,-0.00120815190600194));
#8841=CARTESIAN_POINT('',(0.0151554445662277,0.00200000000000005,0.00875));
#8842=CARTESIAN_POINT('',(0.0092792987869721,0.002,-0.000988520769651722));
#8843=CARTESIAN_POINT('',(0.00585442937138308,0.00200000000000003,0.00237455364019456));
#8844=CARTESIAN_POINT('',(0.0128246445830229,0.002,-0.00228279526592331));
#8845=CARTESIAN_POINT('',(0.00840692818609363,0.002,-0.000405621369795907));
#8846=CARTESIAN_POINT('',(0.0151554445662277,0.00200000000000005,0.00875));
#8847=CARTESIAN_POINT('',(0.00805843799478281,0.002,-0.000138215440957164));
#8848=CARTESIAN_POINT('',(0.00510183810869068,0.00200000000000003,0.00364312256477043));
#8849=CARTESIAN_POINT('',(0.0114045161443848,0.002,-0.00188417772635469));
#8850=CARTESIAN_POINT('',(0.0072696142844388,0.002,0.000553564386465144));
#8851=CARTESIAN_POINT('',(0.0151554445662277,0.00200000000000005,0.00875));
#8852=CARTESIAN_POINT('',(0.0069590089526929,0.002,0.000864169718211046));
#8853=CARTESIAN_POINT('',(0.00452126683987305,0.00200000000000004,0.00499907157815701));
#8854=CARTESIAN_POINT('',(0.0100485671309982,0.002,-0.00130360645753706));
#8855=CARTESIAN_POINT('',(0.00626722912527059,0.002,0.00165299342855505));
#8856=CARTESIAN_POINT('',(0.0151554445662277,0.00200000000000005,0.00875));
#8857=CARTESIAN_POINT('',(0.00599982319643184,0.00200000000000003,0.00200148361986588));
#8858=CARTESIAN_POINT('',(0.00412264930030442,0.00200000000000004,0.00641920001679515));
#8859=CARTESIAN_POINT('',(0.00877999820642231,0.002,-0.000551015194844674));
#8860=CARTESIAN_POINT('',(0.00541692379657602,0.00200000000000003,0.00287385422074434));
#8861=CARTESIAN_POINT('',(0.0151554445662277,0.00200000000000005,0.00875));
#8862=CARTESIAN_POINT('',(0.0051972926602258,0.00200000000000003,0.00325426650782702));
#8863=CARTESIAN_POINT('',(0.00391280594660448,0.00200000000000004,0.00787920908936577));
#8864=CARTESIAN_POINT('',(0.00762051493667037,0.002,0.000360719016560104));
#8865=CARTESIAN_POINT('',(0.00473324725827826,0.00200000000000003,0.00419525749639209));
#8866=CARTESIAN_POINT('',(0.0151554445662277,0.00200000000000005,0.00875));
#8867=CARTESIAN_POINT('',(0.00456514886405276,0.00200000000000003,0.00460108291954443));
#8868=CARTESIAN_POINT('',(0.0038953272567346,0.00200000000000005,0.00935411763584619));
#8869=CARTESIAN_POINT('',(0.00658995640195732,0.002,0.00141599615153965));
#8870=CARTESIAN_POINT('',(0.0042278974054985,0.00200000000000004,0.00559459367908977));
#8871=CARTESIAN_POINT('',(0.0151554445662277,0.00200000000000005,0.00875));
#8872=CARTESIAN_POINT('',(0.00411420796352861,0.00200000000000004,0.00601888845280556));
#8873=CARTESIAN_POINT('',(0.00407051229592446,0.00200000000000005,0.0108186895620842));
#8874=CARTESIAN_POINT('',(0.00570595574453691,0.00200000000000003,0.00259676012573636));
#8875=CARTESIAN_POINT('',(0.00390952091432728,0.00200000000000004,0.00704791973878213));
#8876=CARTESIAN_POINT('',(0.0151554445662277,0.00200000000000005,0.00875));
#8877=CARTESIAN_POINT('',(0.00385218568248577,0.00200000000000004,0.00748342406184637));
#8878=CARTESIAN_POINT('',(0.00443536359958305,0.00200000000000006,0.0122478656363659));
#10141=MECHANICAL_DESIGN_GEOMETRIC_PRESENTATION_REPRESENTATION('',(#5555),#10142);
#10142=(
GEOMETRIC_REPRESENTATION_CONTEXT(3)
GLOBAL_UNCERTAINTY_ASSIGNED_CONTEXT((#10158))
GLOBAL_UNIT_ASSIGNED_CONTEXT((#10176,#10175,#10174))
REPRESENTATION_CONTEXT('MAS-674','TOP_LEVEL_ASSEMBLY_PART')
);
#10145=(
GEOMETRIC_REPRESENTATION_CONTEXT(3)
GLOBAL_UNCERTAINTY_ASSIGNED_CONTEXT((#10161))
GLOBAL_UNIT_ASSIGNED_CONTEXT((#10176,#10175,#10174))
REPRESENTATION_CONTEXT('Part 1','COMPONENT_PART')
);
#10158=UNCERTAINTY_MEASURE_WITH_UNIT(LENGTH_MEASURE(1.E-8),#10176,
'DISTANCE_ACCURACY_VALUE','Maximum Tolerance applied to model');
#10161=UNCERTAINTY_MEASURE_WITH_UNIT(LENGTH_MEASURE(1.E-8),#10176,
'DISTANCE_ACCURACY_VALUE','Maximum Tolerance applied to model');
#10174=(
NAMED_UNIT(*)
SI_UNIT($,.STERADIAN.)
SOLID_ANGLE_UNIT()
);
#10175=(
NAMED_UNIT(*)
PLANE_ANGLE_UNIT()
SI_UNIT($,.RADIAN.)
);
#10176=(
LENGTH_UNIT()
NAMED_UNIT(*)
SI_UNIT($,.METRE.)
);
#10183=PRODUCT_DEFINITION_SHAPE('','',#10213);
#10213=PRODUCT_DEFINITION('','',#10245,#10229);
#10229=PRODUCT_DEFINITION_CONTEXT('',#10323,'design');
#10245=PRODUCT_DEFINITION_FORMATION_WITH_SPECIFIED_SOURCE('','',#10277,
 .NOT_KNOWN.);
#10277=PRODUCT('Part 1','Part 1','Part 1',(#10309));
#10309=PRODUCT_CONTEXT('',#10323,'mechanical');
#10323=APPLICATION_CONTEXT('managed model based 3d engineering');
ENDSEC;
END-ISO-10303-21;
